ISO-10303-21;
HEADER;
/* Generated by software containing ST-Developer
 * from STEP Tools, Inc. (www.steptools.com) 
 */

FILE_DESCRIPTION(
/* description */ (''),
/* implementation_level */ '2;1');

FILE_NAME(
/* name */ 'ISO 1207 - M4 x 8 - 4.8 (Lock Clamp Screw, slotted cheese head).step',
/* time_stamp */ '2026-10-05T09:57:53+05:00',
/* author */ (''),
/* organization */ (''),
/* preprocessor_version */ 'ST-DEVELOPER v20.2',
/* originating_system */ 'Autodesk Translation Framework v15.15.0.0',
/* authorisation */ '');

FILE_SCHEMA (('AUTOMOTIVE_DESIGN { 1 0 10303 214 3 1 1 }'));
ENDSEC;

DATA;
#10=MECHANICAL_DESIGN_GEOMETRIC_PRESENTATION_REPRESENTATION('',(#561),#113984);
#107=TOROIDAL_SURFACE('',#63090,2.154,0.2);
#379=(
BOUNDED_CURVE()
B_SPLINE_CURVE(2,(#104379,#104380,#104381),.UNSPECIFIED.,.F.,.F.)
B_SPLINE_CURVE_WITH_KNOTS((3,3),(0.,0.0570518843466932),.UNSPECIFIED.)
CURVE()
GEOMETRIC_REPRESENTATION_ITEM()
RATIONAL_B_SPLINE_CURVE((1.,1.00190501274853,1.))
REPRESENTATION_ITEM('')
);
#380=(
BOUNDED_CURVE()
B_SPLINE_CURVE(2,(#104384,#104385,#104386),.UNSPECIFIED.,.F.,.F.)
B_SPLINE_CURVE_WITH_KNOTS((3,3),(0.,0.0570518843466932),.UNSPECIFIED.)
CURVE()
GEOMETRIC_REPRESENTATION_ITEM()
RATIONAL_B_SPLINE_CURVE((1.,1.00190501274853,1.))
REPRESENTATION_ITEM('')
);
#381=(
BOUNDED_CURVE()
B_SPLINE_CURVE(2,(#104392,#104393,#104394),.UNSPECIFIED.,.F.,.F.)
B_SPLINE_CURVE_WITH_KNOTS((3,3),(0.,0.0570518843466932),.UNSPECIFIED.)
CURVE()
GEOMETRIC_REPRESENTATION_ITEM()
RATIONAL_B_SPLINE_CURVE((1.,1.00190501272047,1.))
REPRESENTATION_ITEM('')
);
#382=(
BOUNDED_CURVE()
B_SPLINE_CURVE(2,(#104398,#104399,#104400),.UNSPECIFIED.,.F.,.F.)
B_SPLINE_CURVE_WITH_KNOTS((3,3),(0.,0.0570518843466932),.UNSPECIFIED.)
CURVE()
GEOMETRIC_REPRESENTATION_ITEM()
RATIONAL_B_SPLINE_CURVE((1.,1.00190501272047,1.))
REPRESENTATION_ITEM('')
);
#525=SHAPE_REPRESENTATION_RELATIONSHIP('SRR','None',#114062,#543);
#543=ADVANCED_BREP_SHAPE_REPRESENTATION('',(#579),#113976);
#561=STYLED_ITEM('',(#114317),#579);
#579=MANIFOLD_SOLID_BREP(
'ISO 1207 - M4 x 8 - 4.8 (Lock Clamp Screw, slotted cheese head)',#60402);
#718=CYLINDRICAL_SURFACE('',#63059,1.954);
#719=CYLINDRICAL_SURFACE('',#63061,1.954);
#720=CYLINDRICAL_SURFACE('',#63062,1.954);
#721=CYLINDRICAL_SURFACE('',#63063,1.954);
#722=CYLINDRICAL_SURFACE('',#63064,1.954);
#723=CYLINDRICAL_SURFACE('',#63065,1.954);
#724=CYLINDRICAL_SURFACE('',#63066,1.954);
#725=CYLINDRICAL_SURFACE('',#63067,1.954);
#726=CYLINDRICAL_SURFACE('',#63068,1.954);
#727=CYLINDRICAL_SURFACE('',#63069,1.954);
#728=CYLINDRICAL_SURFACE('',#63070,1.954);
#729=CYLINDRICAL_SURFACE('',#63071,1.5555);
#730=CYLINDRICAL_SURFACE('',#63073,1.5555);
#731=CYLINDRICAL_SURFACE('',#63074,1.5555);
#732=CYLINDRICAL_SURFACE('',#63075,1.5555);
#733=CYLINDRICAL_SURFACE('',#63076,1.5555);
#734=CYLINDRICAL_SURFACE('',#63077,1.5555);
#735=CYLINDRICAL_SURFACE('',#63078,1.5555);
#736=CYLINDRICAL_SURFACE('',#63079,1.5555);
#737=CYLINDRICAL_SURFACE('',#63080,1.5555);
#738=CYLINDRICAL_SURFACE('',#63081,1.5555);
#739=CYLINDRICAL_SURFACE('',#63089,1.5555);
#740=CYLINDRICAL_SURFACE('',#63095,1.954);
#741=CYLINDRICAL_SURFACE('',#63111,3.5);
#930=CONICAL_SURFACE('',#63103,3.29999999999998,0.78539816339746);
#931=CONICAL_SURFACE('',#63106,3.29999999999998,0.78539816339746);
#932=CONICAL_SURFACE('',#63112,1.75000000000001,0.785398163397437);
#1284=CIRCLE('',#63060,1.954);
#1285=CIRCLE('',#63072,1.5555);
#1286=CIRCLE('',#63083,1.954);
#1287=CIRCLE('',#63084,1.954);
#1288=CIRCLE('',#63086,1.954);
#1289=CIRCLE('',#63087,1.5555);
#1290=CIRCLE('',#63088,1.954);
#1291=CIRCLE('',#63091,2.154);
#1292=CIRCLE('',#63092,0.2);
#1293=CIRCLE('',#63094,3.5);
#1294=CIRCLE('',#63096,1.954);
#1295=CIRCLE('',#63100,3.5);
#1296=CIRCLE('',#63101,3.5);
#1297=CIRCLE('',#63102,3.5);
#1298=CIRCLE('',#63104,3.5);
#1299=CIRCLE('',#63105,3.09999999999999);
#1300=CIRCLE('',#63107,3.09999999999999);
#1301=CIRCLE('',#63108,3.5);
#1302=CIRCLE('',#63113,1.5);
#1851=FACE_BOUND('',#10454,.T.);
#3784=PLANE('',#63082);
#3785=PLANE('',#63085);
#3786=PLANE('',#63093);
#3787=PLANE('',#63097);
#3788=PLANE('',#63098);
#3789=PLANE('',#63099);
#3790=PLANE('',#63109);
#3791=PLANE('',#63110);
#3792=PLANE('',#63114);
#6850=FACE_OUTER_BOUND('',#10426,.T.);
#6851=FACE_OUTER_BOUND('',#10427,.T.);
#6852=FACE_OUTER_BOUND('',#10428,.T.);
#6853=FACE_OUTER_BOUND('',#10429,.T.);
#6854=FACE_OUTER_BOUND('',#10430,.T.);
#6855=FACE_OUTER_BOUND('',#10431,.T.);
#6856=FACE_OUTER_BOUND('',#10432,.T.);
#6857=FACE_OUTER_BOUND('',#10433,.T.);
#6858=FACE_OUTER_BOUND('',#10434,.T.);
#6859=FACE_OUTER_BOUND('',#10435,.T.);
#6860=FACE_OUTER_BOUND('',#10436,.T.);
#6861=FACE_OUTER_BOUND('',#10437,.T.);
#6862=FACE_OUTER_BOUND('',#10438,.T.);
#6863=FACE_OUTER_BOUND('',#10439,.T.);
#6864=FACE_OUTER_BOUND('',#10440,.T.);
#6865=FACE_OUTER_BOUND('',#10441,.T.);
#6866=FACE_OUTER_BOUND('',#10442,.T.);
#6867=FACE_OUTER_BOUND('',#10443,.T.);
#6868=FACE_OUTER_BOUND('',#10444,.T.);
#6869=FACE_OUTER_BOUND('',#10445,.T.);
#6870=FACE_OUTER_BOUND('',#10446,.T.);
#6871=FACE_OUTER_BOUND('',#10447,.T.);
#6872=FACE_OUTER_BOUND('',#10448,.T.);
#6873=FACE_OUTER_BOUND('',#10449,.T.);
#6874=FACE_OUTER_BOUND('',#10450,.T.);
#6875=FACE_OUTER_BOUND('',#10451,.T.);
#6876=FACE_OUTER_BOUND('',#10452,.T.);
#6877=FACE_OUTER_BOUND('',#10453,.T.);
#6878=FACE_OUTER_BOUND('',#10455,.T.);
#6879=FACE_OUTER_BOUND('',#10456,.T.);
#6880=FACE_OUTER_BOUND('',#10457,.T.);
#6881=FACE_OUTER_BOUND('',#10458,.T.);
#6882=FACE_OUTER_BOUND('',#10459,.T.);
#6883=FACE_OUTER_BOUND('',#10460,.T.);
#6884=FACE_OUTER_BOUND('',#10461,.T.);
#6885=FACE_OUTER_BOUND('',#10462,.T.);
#6886=FACE_OUTER_BOUND('',#10463,.T.);
#6887=FACE_OUTER_BOUND('',#10464,.T.);
#6888=FACE_OUTER_BOUND('',#10465,.T.);
#10426=EDGE_LOOP('',(#54091,#54092,#54093,#54094));
#10427=EDGE_LOOP('',(#54095,#54096,#54097,#54098));
#10428=EDGE_LOOP('',(#54099,#54100,#54101,#54102));
#10429=EDGE_LOOP('',(#54103,#54104,#54105,#54106));
#10430=EDGE_LOOP('',(#54107,#54108,#54109,#54110));
#10431=EDGE_LOOP('',(#54111,#54112,#54113,#54114));
#10432=EDGE_LOOP('',(#54115,#54116,#54117,#54118));
#10433=EDGE_LOOP('',(#54119,#54120,#54121,#54122));
#10434=EDGE_LOOP('',(#54123,#54124,#54125,#54126));
#10435=EDGE_LOOP('',(#54127,#54128,#54129,#54130));
#10436=EDGE_LOOP('',(#54131,#54132,#54133,#54134));
#10437=EDGE_LOOP('',(#54135,#54136,#54137,#54138));
#10438=EDGE_LOOP('',(#54139,#54140,#54141,#54142));
#10439=EDGE_LOOP('',(#54143,#54144,#54145,#54146));
#10440=EDGE_LOOP('',(#54147,#54148,#54149,#54150));
#10441=EDGE_LOOP('',(#54151,#54152,#54153,#54154));
#10442=EDGE_LOOP('',(#54155,#54156,#54157,#54158));
#10443=EDGE_LOOP('',(#54159,#54160,#54161,#54162));
#10444=EDGE_LOOP('',(#54163,#54164,#54165,#54166));
#10445=EDGE_LOOP('',(#54167,#54168,#54169,#54170));
#10446=EDGE_LOOP('',(#54171,#54172,#54173,#54174));
#10447=EDGE_LOOP('',(#54175,#54176,#54177,#54178,#54179));
#10448=EDGE_LOOP('',(#54180,#54181,#54182,#54183,#54184,#54185,#54186,#54187,
#54188,#54189,#54190,#54191,#54192,#54193,#54194,#54195,#54196,#54197,#54198,
#54199,#54200,#54201,#54202,#54203,#54204));
#10449=EDGE_LOOP('',(#54205,#54206,#54207,#54208,#54209));
#10450=EDGE_LOOP('',(#54210,#54211,#54212,#54213));
#10451=EDGE_LOOP('',(#54214,#54215,#54216,#54217,#54218,#54219,#54220,#54221,
#54222,#54223,#54224,#54225,#54226,#54227,#54228,#54229,#54230,#54231,#54232,
#54233,#54234,#54235,#54236,#54237,#54238));
#10452=EDGE_LOOP('',(#54239,#54240,#54241,#54242,#54243,#54244));
#10453=EDGE_LOOP('',(#54245));
#10454=EDGE_LOOP('',(#54246));
#10455=EDGE_LOOP('',(#54247,#54248,#54249,#54250));
#10456=EDGE_LOOP('',(#54251,#54252,#54253,#54254,#54255,#54256));
#10457=EDGE_LOOP('',(#54257,#54258,#54259,#54260,#54261,#54262));
#10458=EDGE_LOOP('',(#54263,#54264,#54265,#54266,#54267));
#10459=EDGE_LOOP('',(#54268,#54269,#54270,#54271));
#10460=EDGE_LOOP('',(#54272,#54273,#54274,#54275));
#10461=EDGE_LOOP('',(#54276,#54277));
#10462=EDGE_LOOP('',(#54278,#54279));
#10463=EDGE_LOOP('',(#54280,#54281,#54282,#54283,#54284,#54285,#54286,#54287,
#54288,#54289,#54290,#54291));
#10464=EDGE_LOOP('',(#54292,#54293,#54294,#54295,#54296,#54297));
#10465=EDGE_LOOP('',(#54298));
#16416=LINE('',#102632,#22450);
#16417=LINE('',#102656,#22451);
#16418=LINE('',#102704,#22452);
#16419=LINE('',#102752,#22453);
#16420=LINE('',#102806,#22454);
#16421=LINE('',#102854,#22455);
#16422=LINE('',#102908,#22456);
#16423=LINE('',#102956,#22457);
#16424=LINE('',#103004,#22458);
#16425=LINE('',#103058,#22459);
#16426=LINE('',#103106,#22460);
#16427=LINE('',#103154,#22461);
#16428=LINE('',#103178,#22462);
#16429=LINE('',#103202,#22463);
#16430=LINE('',#103227,#22464);
#16431=LINE('',#103252,#22465);
#16432=LINE('',#103276,#22466);
#16433=LINE('',#103301,#22467);
#16434=LINE('',#103326,#22468);
#16435=LINE('',#103351,#22469);
#16436=LINE('',#103376,#22470);
#16437=LINE('',#104373,#22471);
#16438=LINE('',#104375,#22472);
#16439=LINE('',#104377,#22473);
#16440=LINE('',#104383,#22474);
#16441=LINE('',#104390,#22475);
#16442=LINE('',#104396,#22476);
#16443=LINE('',#104402,#22477);
#16444=LINE('',#104403,#22478);
#16445=LINE('',#104418,#22479);
#16446=LINE('',#104422,#22480);
#22450=VECTOR('',#74218,1.99999999999999);
#22451=VECTOR('',#74223,1.99999999999999);
#22452=VECTOR('',#74226,1.99999999999999);
#22453=VECTOR('',#74229,1.99999999999999);
#22454=VECTOR('',#74232,1.99999999999999);
#22455=VECTOR('',#74235,1.99999999999999);
#22456=VECTOR('',#74238,1.99999999999999);
#22457=VECTOR('',#74241,1.99999999999999);
#22458=VECTOR('',#74244,1.99999999999999);
#22459=VECTOR('',#74247,1.99999999999999);
#22460=VECTOR('',#74250,1.99999999999999);
#22461=VECTOR('',#74253,1.5555);
#22462=VECTOR('',#74258,1.5555);
#22463=VECTOR('',#74261,1.5555);
#22464=VECTOR('',#74264,1.5555);
#22465=VECTOR('',#74267,1.5555);
#22466=VECTOR('',#74270,1.5555);
#22467=VECTOR('',#74273,1.5555);
#22468=VECTOR('',#74276,1.5555);
#22469=VECTOR('',#74279,1.5555);
#22470=VECTOR('',#74282,1.5555);
#22471=VECTOR('',#74315,10.);
#22472=VECTOR('',#74316,10.);
#22473=VECTOR('',#74317,10.);
#22474=VECTOR('',#74318,10.);
#22475=VECTOR('',#74321,10.);
#22476=VECTOR('',#74322,10.);
#22477=VECTOR('',#74323,10.);
#22478=VECTOR('',#74324,10.);
#22479=VECTOR('',#74351,3.5);
#22480=VECTOR('',#74356,1.75000000000001);
#24350=B_SPLINE_CURVE_WITH_KNOTS('',3,(#102634,#102635,#102636,#102637,
#102638,#102639,#102640,#102641,#102642,#102643),.UNSPECIFIED.,.F.,.F.,
(4,3,3,4),(-4.09254174883833,-3.9421844604419,-2.95663834533143,-2.06514013327814),
 .UNSPECIFIED.);
#24351=B_SPLINE_CURVE_WITH_KNOTS('',3,(#102646,#102647,#102648,#102649,
#102650,#102651,#102652),.UNSPECIFIED.,.F.,.F.,(4,3,4),(0.,0.985546115110468,
1.11419103802957),.UNSPECIFIED.);
#24352=B_SPLINE_CURVE_WITH_KNOTS('',3,(#102657,#102658,#102659,#102660,
#102661,#102662,#102663,#102664,#102665,#102666,#102667,#102668,#102669,
#102670,#102671,#102672,#102673,#102674,#102675,#102676,#102677,#102678),
 .UNSPECIFIED.,.F.,.F.,(4,3,3,3,3,3,3,4),(-10.3757270560179,-9.85546115110475,
-8.86991503599427,-7.8843689208838,-6.89882280577333,-5.91327669066285,
-4.92773057555237,-4.09254174883833),.UNSPECIFIED.);
#24353=B_SPLINE_CURVE_WITH_KNOTS('',3,(#102679,#102680,#102681,#102682,
#102683,#102684,#102685,#102686,#102687,#102688,#102689,#102690,#102691,
#102692,#102693,#102694,#102695,#102696,#102697,#102698,#102699,#102700),
 .UNSPECIFIED.,.F.,.F.,(4,3,3,3,3,3,3,4),(1.11419103802957,1.97109223022095,
2.95663834533142,3.9421844604419,4.92773057555238,5.91327669066286,6.89882280577334,
7.39737634520915),.UNSPECIFIED.);
#24354=B_SPLINE_CURVE_WITH_KNOTS('',3,(#102705,#102706,#102707,#102708,
#102709,#102710,#102711,#102712,#102713,#102714,#102715,#102716,#102717,
#102718,#102719,#102720,#102721,#102722,#102723,#102724,#102725,#102726),
 .UNSPECIFIED.,.F.,.F.,(4,3,3,3,3,3,3,4),(-16.6589123631975,-15.7687378417676,
-14.7831917266571,-13.7976456115466,-12.8120994964362,-11.8265533813257,
-10.8410072662152,-10.3757270560179),.UNSPECIFIED.);
#24355=B_SPLINE_CURVE_WITH_KNOTS('',3,(#102727,#102728,#102729,#102730,
#102731,#102732,#102733,#102734,#102735,#102736,#102737,#102738,#102739,
#102740,#102741,#102742,#102743,#102744,#102745,#102746,#102747,#102748),
 .UNSPECIFIED.,.F.,.F.,(4,3,3,3,3,3,3,4),(7.39737634520915,7.88436892088381,
8.86991503599429,9.85546115110476,10.8410072662152,11.8265533813257,12.8120994964362,
13.6805616523887),.UNSPECIFIED.);
#24356=B_SPLINE_CURVE_WITH_KNOTS('',3,(#102753,#102754,#102755,#102756,
#102757,#102758,#102759,#102760,#102761,#102762,#102763,#102764,#102765,
#102766,#102767,#102768,#102769,#102770,#102771,#102772,#102773,#102774,
#102775,#102776,#102777),.UNSPECIFIED.,.F.,.F.,(4,3,3,3,3,3,3,3,4),(-22.9420976703771,
-22.6675606475409,-21.6820145324305,-20.69646841732,-19.7109223022095,-18.725376187099,
-17.7398300719886,-16.7542839568781,-16.6589123631975),.UNSPECIFIED.);
#24357=B_SPLINE_CURVE_WITH_KNOTS('',3,(#102778,#102779,#102780,#102781,
#102782,#102783,#102784,#102785,#102786,#102787,#102788,#102789,#102790,
#102791,#102792,#102793,#102794,#102795,#102796,#102797,#102798,#102799,
#102800,#102801,#102802),.UNSPECIFIED.,.F.,.F.,(4,3,3,3,3,3,3,3,4),(13.6805616523887,
13.7976456115467,14.7831917266571,15.7687378417676,16.7542839568781,17.7398300719886,
18.725376187099,19.7109223022095,19.9637469595683),.UNSPECIFIED.);
#24358=B_SPLINE_CURVE_WITH_KNOTS('',3,(#102807,#102808,#102809,#102810,
#102811,#102812,#102813,#102814,#102815,#102816,#102817,#102818,#102819,
#102820,#102821,#102822,#102823,#102824,#102825,#102826,#102827,#102828),
 .UNSPECIFIED.,.F.,.F.,(4,3,3,3,3,3,3,4),(-29.2252829775567,-28.5808373382038,
-27.5952912230933,-26.6097451079828,-25.6241989928724,-24.6386528777619,
-23.6531067626514,-22.9420976703771),.UNSPECIFIED.);
#24359=B_SPLINE_CURVE_WITH_KNOTS('',3,(#102829,#102830,#102831,#102832,
#102833,#102834,#102835,#102836,#102837,#102838,#102839,#102840,#102841,
#102842,#102843,#102844,#102845,#102846,#102847,#102848,#102849,#102850),
 .UNSPECIFIED.,.F.,.F.,(4,3,3,3,3,3,3,4),(19.9637469595683,20.69646841732,
21.6820145324305,22.6675606475409,23.6531067626514,24.6386528777619,25.6241989928724,
26.2469322667479),.UNSPECIFIED.);
#24360=B_SPLINE_CURVE_WITH_KNOTS('',3,(#102855,#102856,#102857,#102858,
#102859,#102860,#102861,#102862,#102863,#102864,#102865,#102866,#102867,
#102868,#102869,#102870,#102871,#102872,#102873,#102874,#102875,#102876,
#102877,#102878,#102879),.UNSPECIFIED.,.F.,.F.,(4,3,3,3,3,3,3,3,4),(-35.5084682847363,
-35.4796601439771,-34.4941140288666,-33.5085679137561,-32.5230217986457,
-31.5374756835352,-30.5519295684247,-29.5663834533142,-29.2252829775567),
 .UNSPECIFIED.);
#24361=B_SPLINE_CURVE_WITH_KNOTS('',3,(#102880,#102881,#102882,#102883,
#102884,#102885,#102886,#102887,#102888,#102889,#102890,#102891,#102892,
#102893,#102894,#102895,#102896,#102897,#102898,#102899,#102900,#102901,
#102902,#102903,#102904),.UNSPECIFIED.,.F.,.F.,(4,3,3,3,3,3,3,3,4),(26.2469322667479,
26.6097451079828,27.5952912230933,28.5808373382038,29.5663834533142,30.5519295684247,
31.5374756835352,32.5230217986457,32.5301175739275),.UNSPECIFIED.);
#24362=B_SPLINE_CURVE_WITH_KNOTS('',3,(#102909,#102910,#102911,#102912,
#102913,#102914,#102915,#102916,#102917,#102918,#102919,#102920,#102921,
#102922,#102923,#102924,#102925,#102926,#102927,#102928,#102929,#102930),
 .UNSPECIFIED.,.F.,.F.,(4,3,3,3,3,3,3,4),(-41.7916535919158,-41.3929368346399,
-40.4073907195295,-39.421844604419,-38.4362984893085,-37.450752374198,-36.4652062590876,
-35.5084682847363),.UNSPECIFIED.);
#24363=B_SPLINE_CURVE_WITH_KNOTS('',3,(#102931,#102932,#102933,#102934,
#102935,#102936,#102937,#102938,#102939,#102940,#102941,#102942,#102943,
#102944,#102945,#102946,#102947,#102948,#102949,#102950,#102951,#102952),
 .UNSPECIFIED.,.F.,.F.,(4,3,3,3,3,3,3,4),(32.5301175739275,33.5085679137562,
34.4941140288666,35.4796601439771,36.4652062590876,37.4507523741981,38.4362984893085,
38.8133028811071),.UNSPECIFIED.);
#24364=B_SPLINE_CURVE_WITH_KNOTS('',3,(#102957,#102958,#102959,#102960,
#102961,#102962,#102963,#102964,#102965,#102966,#102967,#102968,#102969,
#102970,#102971,#102972,#102973,#102974,#102975,#102976,#102977,#102978),
 .UNSPECIFIED.,.F.,.F.,(4,3,3,3,3,3,3,4),(-48.0748388990954,-47.3062135253028,
-46.3206674101923,-45.3351212950818,-44.3495751799714,-43.3640290648609,
-42.3784829497504,-41.7916535919158),.UNSPECIFIED.);
#24365=B_SPLINE_CURVE_WITH_KNOTS('',3,(#102979,#102980,#102981,#102982,
#102983,#102984,#102985,#102986,#102987,#102988,#102989,#102990,#102991,
#102992,#102993,#102994,#102995,#102996,#102997,#102998,#102999,#103000),
 .UNSPECIFIED.,.F.,.F.,(4,3,3,3,3,3,3,4),(38.8133028811071,39.421844604419,
40.4073907195295,41.39293683464,42.3784829497504,43.3640290648609,44.3495751799714,
45.0964881882867),.UNSPECIFIED.);
#24366=B_SPLINE_CURVE_WITH_KNOTS('',3,(#103005,#103006,#103007,#103008,
#103009,#103010,#103011,#103012,#103013,#103014,#103015,#103016,#103017,
#103018,#103019,#103020,#103021,#103022,#103023,#103024,#103025,#103026,
#103027,#103028,#103029),.UNSPECIFIED.,.F.,.F.,(4,3,3,3,3,3,3,3,4),(-54.358024206275,
-54.2050363310761,-53.2194902159656,-52.2339441008552,-51.2483979857447,
-50.2628518706342,-49.2773057555237,-48.2917596404133,-48.0748388990954),
 .UNSPECIFIED.);
#24367=B_SPLINE_CURVE_WITH_KNOTS('',3,(#103030,#103031,#103032,#103033,
#103034,#103035,#103036,#103037,#103038,#103039,#103040,#103041,#103042,
#103043,#103044,#103045,#103046,#103047,#103048,#103049,#103050,#103051,
#103052,#103053,#103054),.UNSPECIFIED.,.F.,.F.,(4,3,3,3,3,3,3,3,4),(45.0964881882867,
45.3351212950819,46.3206674101923,47.3062135253028,48.2917596404133,49.2773057555238,
50.2628518706342,51.2483979857447,51.3796734954663),.UNSPECIFIED.);
#24368=B_SPLINE_CURVE_WITH_KNOTS('',3,(#103059,#103060,#103061,#103062,
#103063,#103064,#103065,#103066,#103067,#103068,#103069,#103070,#103071,
#103072,#103073,#103074,#103075,#103076,#103077,#103078,#103079,#103080),
 .UNSPECIFIED.,.F.,.F.,(4,3,3,3,3,3,3,4),(-60.6412095134546,-60.118313021739,
-59.1327669066285,-58.147220791518,-57.1616746764076,-56.1761285612971,
-55.1905824461866,-54.358024206275),.UNSPECIFIED.);
#24369=B_SPLINE_CURVE_WITH_KNOTS('',3,(#103081,#103082,#103083,#103084,
#103085,#103086,#103087,#103088,#103089,#103090,#103091,#103092,#103093,
#103094,#103095,#103096,#103097,#103098,#103099,#103100,#103101,#103102),
 .UNSPECIFIED.,.F.,.F.,(4,3,3,3,3,3,3,4),(51.3796734954663,52.2339441008552,
53.2194902159657,54.2050363310761,55.1905824461866,56.1761285612971,57.1616746764076,
57.6628588026459),.UNSPECIFIED.);
#24370=B_SPLINE_CURVE_WITH_KNOTS('',3,(#103107,#103108,#103109,#103110,
#103111,#103112,#103113,#103114,#103115,#103116,#103117,#103118,#103119,
#103120,#103121,#103122,#103123,#103124,#103125,#103126,#103127,#103128),
 .UNSPECIFIED.,.F.,.F.,(4,3,3,3,3,3,3,4),(-66.9243948206342,-66.0315897124018,
-65.0460435972913,-64.0604974821809,-63.0749513670704,-62.0894052519599,
-61.1038591368495,-60.6412095134546),.UNSPECIFIED.);
#24371=B_SPLINE_CURVE_WITH_KNOTS('',3,(#103129,#103130,#103131,#103132,
#103133,#103134,#103135,#103136,#103137,#103138,#103139,#103140,#103141,
#103142,#103143,#103144,#103145,#103146,#103147,#103148,#103149,#103150),
 .UNSPECIFIED.,.F.,.F.,(4,3,3,3,3,3,3,4),(57.6628588026459,58.147220791518,
59.1327669066285,60.118313021739,61.1038591368495,62.0894052519599,63.0749513670704,
63.9460441098255),.UNSPECIFIED.);
#24372=B_SPLINE_CURVE_WITH_KNOTS('',3,(#103156,#103157,#103158,#103159,
#103160,#103161,#103162,#103163,#103164),.UNSPECIFIED.,.F.,.F.,(4,1,1,1,
1,1,4),(72.2566310325653,72.71928065596,73.7048267710705,74.690372886181,
75.6759190012915,76.6614651164019,77.5529633284553),.UNSPECIFIED.);
#24373=B_SPLINE_CURVE_WITH_KNOTS('',3,(#103167,#103168,#103169,#103170,
#103171,#103172,#103173,#103174),.UNSPECIFIED.,.F.,.F.,(4,1,1,1,1,4),(72.2566310325652,
72.3710844049206,73.3566305200311,74.3421766351416,75.327722750252,76.3132688653625),
 .UNSPECIFIED.);
#24374=B_SPLINE_CURVE_WITH_KNOTS('',3,(#103179,#103180,#103181,#103182,
#103183,#103184,#103185,#103186,#103187,#103188),.UNSPECIFIED.,.F.,.F.,
(4,1,1,1,1,1,1,4),(65.9734457253856,66.8060039652972,67.7915500804077,68.7770961955181,
69.7626423106286,70.7481884257391,71.7337345408496,72.2566310325653),
 .UNSPECIFIED.);
#24375=B_SPLINE_CURVE_WITH_KNOTS('',3,(#103189,#103190,#103191,#103192,
#103193,#103194,#103195,#103196,#103197,#103198),.UNSPECIFIED.,.F.,.F.,
(4,1,1,1,1,1,1,4),(65.9734457253856,66.4578077142578,67.4433538293682,68.4288999444787,
69.4144460595892,70.3999921746997,71.3855382898101,72.2566310325652),
 .UNSPECIFIED.);
#24376=B_SPLINE_CURVE_WITH_KNOTS('',3,(#103203,#103204,#103205,#103206,
#103207,#103208,#103209,#103210,#103211,#103212,#103213),.UNSPECIFIED.,
 .F.,.F.,(4,1,1,1,1,1,1,1,4),(59.6902604182061,59.9071811595239,60.8927272746343,
61.8782733897448,62.8638195048553,63.8493656199658,64.8349117350762,65.8204578501867,
65.9734457253856),.UNSPECIFIED.);
#24377=B_SPLINE_CURVE_WITH_KNOTS('',3,(#103214,#103215,#103216,#103217,
#103218,#103219,#103220,#103221,#103222,#103223),.UNSPECIFIED.,.F.,.F.,
(4,1,1,1,1,1,1,4),(59.6902604182061,60.5445310235949,61.5300771387054,62.5156232538159,
63.5011693689263,64.4867154840368,65.4722615991473,65.9734457253856),
 .UNSPECIFIED.);
#24378=B_SPLINE_CURVE_WITH_KNOTS('',3,(#103228,#103229,#103230,#103231,
#103232,#103233,#103234,#103235,#103236,#103237),.UNSPECIFIED.,.F.,.F.,
(4,1,1,1,1,1,1,4),(53.4070751110265,53.993904468861,54.9794505839715,55.964996699082,
56.9505428141924,57.9360889293029,58.9216350444134,59.6902604182061),
 .UNSPECIFIED.);
#24379=B_SPLINE_CURVE_WITH_KNOTS('',3,(#103238,#103239,#103240,#103241,
#103242,#103243,#103244,#103245,#103246,#103247,#103248),.UNSPECIFIED.,
 .F.,.F.,(4,1,1,1,1,1,1,1,4),(53.4070751110265,53.6457082178216,54.6312543329321,
55.6168004480425,56.602346563153,57.5878926782635,58.573438793374,59.5589849084844,
59.6902604182061),.UNSPECIFIED.);
#24380=B_SPLINE_CURVE_WITH_KNOTS('',3,(#103253,#103254,#103255,#103256,
#103257,#103258,#103259,#103260,#103261,#103262),.UNSPECIFIED.,.F.,.F.,
(4,1,1,1,1,1,1,4),(47.1238898038469,48.0806277781982,49.0661738933086,50.0517200084191,
51.0372661235296,52.0228122386401,53.0083583537505,53.4070751110265),
 .UNSPECIFIED.);
#24381=B_SPLINE_CURVE_WITH_KNOTS('',3,(#103263,#103264,#103265,#103266,
#103267,#103268,#103269,#103270,#103271,#103272),.UNSPECIFIED.,.F.,.F.,
(4,1,1,1,1,1,1,4),(47.1238898038469,47.7324315271587,48.7179776422692,49.7035237573797,
50.6890698724902,51.6746159876006,52.6601621027111,53.4070751110265),
 .UNSPECIFIED.);
#24382=B_SPLINE_CURVE_WITH_KNOTS('',3,(#103277,#103278,#103279,#103280,
#103281,#103282,#103283,#103284,#103285,#103286,#103287),.UNSPECIFIED.,
 .F.,.F.,(4,1,1,1,1,1,1,1,4),(40.8407044966673,41.1818049724248,42.1673510875353,
43.1528972026458,44.1384433177563,45.1239894328667,46.1095355479772,47.0950816630877,
47.1238898038469),.UNSPECIFIED.);
#24383=B_SPLINE_CURVE_WITH_KNOTS('',3,(#103288,#103289,#103290,#103291,
#103292,#103293,#103294,#103295,#103296,#103297),.UNSPECIFIED.,.F.,.F.,
(4,1,1,1,1,1,1,4),(40.8407044966673,41.8191548364959,42.8047009516064,43.7902470667168,
44.7757931818273,45.7613392969378,46.7468854120483,47.1238898038469),
 .UNSPECIFIED.);
#24384=B_SPLINE_CURVE_WITH_KNOTS('',3,(#103302,#103303,#103304,#103305,
#103306,#103307,#103308,#103309,#103310,#103311),.UNSPECIFIED.,.F.,.F.,
(4,1,1,1,1,1,1,4),(34.5575191894877,35.268528281762,36.2540743968725,37.2396205119829,
38.2251666270934,39.2107127422039,40.1962588573144,40.8407044966673),
 .UNSPECIFIED.);
#24385=B_SPLINE_CURVE_WITH_KNOTS('',3,(#103312,#103313,#103314,#103315,
#103316,#103317,#103318,#103319,#103320,#103321,#103322),.UNSPECIFIED.,
 .F.,.F.,(4,1,1,1,1,1,1,1,4),(34.5575191894877,34.9203320307226,35.905878145833,
36.8914242609435,37.876970376054,38.8625164911645,39.8480626062749,40.8336087213854,
40.8407044966673),.UNSPECIFIED.);
#24386=B_SPLINE_CURVE_WITH_KNOTS('',3,(#103327,#103328,#103329,#103330,
#103331,#103332,#103333,#103334,#103335,#103336,#103337),.UNSPECIFIED.,
 .F.,.F.,(4,1,1,1,1,1,1,1,4),(28.2743338823081,28.3697054759887,29.3552515910991,
30.3407977062096,31.3263438213201,32.3118899364306,33.297436051541,34.2829821666515,
34.5575191894877),.UNSPECIFIED.);
#24387=B_SPLINE_CURVE_WITH_KNOTS('',3,(#103338,#103339,#103340,#103341,
#103342,#103343,#103344,#103345,#103346,#103347),.UNSPECIFIED.,.F.,.F.,
(4,1,1,1,1,1,1,4),(28.2743338823081,29.0070553400597,29.9926014551702,30.9781475702807,
31.9636936853911,32.9492398005016,33.9347859156121,34.5575191894877),
 .UNSPECIFIED.);
#24388=B_SPLINE_CURVE_WITH_KNOTS('',3,(#103352,#103353,#103354,#103355,
#103356,#103357,#103358,#103359,#103360,#103361),.UNSPECIFIED.,.F.,.F.,
(4,1,1,1,1,1,1,4),(21.9911485751285,22.4564287853258,23.4419749004363,24.4275210155468,
25.4130671306572,26.3986132457677,27.3841593608782,28.2743338823081),
 .UNSPECIFIED.);
#24389=B_SPLINE_CURVE_WITH_KNOTS('',3,(#103362,#103363,#103364,#103365,
#103366,#103367,#103368,#103369,#103370,#103371,#103372),.UNSPECIFIED.,
 .F.,.F.,(4,1,1,1,1,1,1,1,4),(21.9911485751285,22.1082325342864,23.0937786493969,
24.0793247645073,25.0648708796178,26.0504169947283,27.0359631098388,28.0215092249492,
28.2743338823081),.UNSPECIFIED.);
#24390=B_SPLINE_CURVE_WITH_KNOTS('',3,(#103377,#103378,#103379,#103380,
#103381,#103382,#103383,#103384,#103385,#103386),.UNSPECIFIED.,.F.,.F.,
(4,1,1,1,1,1,1,4),(15.7079632679489,16.543152094663,17.5286982097734,18.5142443248839,
19.4997904399944,20.4853365551049,21.4708826702153,21.9911485751285),
 .UNSPECIFIED.);
#24391=B_SPLINE_CURVE_WITH_KNOTS('',3,(#103387,#103388,#103389,#103390,
#103391,#103392,#103393,#103394,#103395,#103396),.UNSPECIFIED.,.F.,.F.,
(4,1,1,1,1,1,1,4),(15.7079632679489,16.1949558436235,17.180501958734,18.1660480738445,
19.151594188955,20.1371403040654,21.1226864191759,21.9911485751285),
 .UNSPECIFIED.);
#24392=B_SPLINE_CURVE_WITH_KNOTS('',3,(#103399,#103400,#103401,#103402,
#103403,#103404,#103405,#103406,#103407,#103408,#103409,#103410,#103411,
#103412,#103413,#103414,#103415,#103416,#103417,#103418,#103419,#103420,
#103421,#103422,#103423,#103424,#103425,#103426,#103427,#103428,#103429,
#103430,#103431,#103432,#103433,#103434,#103435,#103436,#103437,#103438,
#103439,#103440,#103441,#103442,#103443,#103444,#103445,#103446,#103447,
#103448,#103449,#103450,#103451,#103452,#103453,#103454,#103455,#103456,
#103457,#103458,#103459,#103460,#103461,#103462,#103463,#103464,#103465,
#103466,#103467,#103468,#103469,#103470,#103471,#103472,#103473,#103474,
#103475,#103476,#103477,#103478,#103479,#103480,#103481,#103482,#103483),
 .UNSPECIFIED.,.F.,.F.,(4,3,3,3,3,3,3,3,3,3,3,3,3,3,3,3,3,3,3,3,3,3,3,3,
3,3,3,3,4),(-0.366397579005812,-0.351492437457111,-0.333436272682045,-0.327541718423651,
-0.321586762936821,-0.302799537357183,-0.288072678932441,-0.281533577517853,
-0.277630627523778,-0.258213375235538,-0.238401773301456,-0.225047497465903,
-0.215841092287883,-0.212852466676624,-0.192423383237538,-0.184984669959245,
-0.165235867770824,-0.154908626035148,-0.149716784328444,-0.14604205573285,
-0.125631137691432,-0.104768267325392,-0.0837068564958923,-0.0753026362798158,
-0.0721925998946417,-0.0505573660781355,-0.0288673280700796,-0.00763422837764629,
0.),.UNSPECIFIED.);
#24393=B_SPLINE_CURVE_WITH_KNOTS('',3,(#103488,#103489,#103490,#103491,
#103492,#103493,#103494,#103495,#103496,#103497,#103498,#103499,#103500,
#103501,#103502,#103503,#103504,#103505,#103506,#103507,#103508,#103509,
#103510,#103511,#103512,#103513,#103514,#103515,#103516,#103517,#103518,
#103519,#103520,#103521,#103522,#103523,#103524,#103525,#103526,#103527,
#103528,#103529,#103530,#103531,#103532,#103533,#103534,#103535,#103536,
#103537,#103538,#103539,#103540,#103541,#103542,#103543,#103544,#103545,
#103546,#103547,#103548,#103549,#103550,#103551,#103552,#103553,#103554,
#103555,#103556,#103557,#103558,#103559,#103560,#103561,#103562,#103563,
#103564,#103565,#103566,#103567,#103568,#103569,#103570,#103571,#103572),
 .UNSPECIFIED.,.F.,.F.,(4,3,3,3,3,3,3,3,3,3,3,3,3,3,3,3,3,3,3,3,3,3,3,3,
3,3,3,3,4),(-0.364629307890707,-0.346303779262462,-0.324667498644849,-0.315327518859617,
-0.310804290329342,-0.289490472824316,-0.273816300085133,-0.265502635085818,
-0.261675347015529,-0.240939232650462,-0.220671164473983,-0.2065276460832,
-0.194625115085288,-0.191251266670405,-0.171660083226589,-0.164097090910852,
-0.143584954546996,-0.134293385868617,-0.12844412724776,-0.12395210201744,
-0.104508817089354,-0.0851257087077866,-0.066128864910575,-0.0618232941908036,
-0.0586106046312514,-0.040025091744189,-0.0217742516347645,-0.00410398101321869,
0.),.UNSPECIFIED.);
#24394=B_SPLINE_CURVE_WITH_KNOTS('',3,(#103861,#103862,#103863,#103864,
#103865,#103866,#103867,#103868,#103869,#103870),.UNSPECIFIED.,.F.,.F.,
(4,3,3,4),(63.9460441098255,64.0604974821809,65.0460435972913,65.9375418093447),
 .UNSPECIFIED.);
#24395=B_SPLINE_CURVE_WITH_KNOTS('',3,(#103872,#103873,#103874,#103875,
#103876,#103877,#103878,#103879,#103880,#103881,#103882,#103883,#103884,
#103885,#103886,#103887,#103888,#103889,#103890,#103891,#103892,#103893,
#103894,#103895,#103896,#103897,#103898,#103899,#103900,#103901,#103902,
#103903,#103904,#103905,#103906,#103907,#103908,#103909,#103910,#103911,
#103912,#103913,#103914,#103915,#103916,#103917,#103918,#103919,#103920,
#103921,#103922,#103923,#103924,#103925,#103926,#103927,#103928,#103929,
#103930,#103931,#103932,#103933,#103934,#103935,#103936,#103937,#103938,
#103939,#103940,#103941,#103942,#103943,#103944,#103945,#103946,#103947,
#103948,#103949,#103950,#103951,#103952,#103953,#103954,#103955,#103956),
 .UNSPECIFIED.,.F.,.F.,(4,3,3,3,3,3,3,3,3,3,3,3,3,3,3,3,3,3,3,3,3,3,3,3,
3,3,3,3,4),(-0.366397579005849,-0.351492437457149,-0.333436262306682,-0.327541704777944,
-0.321586765496969,-0.302799532896208,-0.288072675029088,-0.281533538088545,
-0.277630621502244,-0.258213363775523,-0.238401762886512,-0.225047489654695,
-0.215841075396366,-0.212852442823409,-0.192423360392375,-0.184984669959245,
-0.165235863076095,-0.154908621633839,-0.149716783504717,-0.146042055985856,
-0.125631132714399,-0.104768256578359,-0.0837068447019094,-0.075302640797004,
-0.072192607079805,-0.050557369643571,-0.0288673349885595,-0.00763425242218924,
0.),.UNSPECIFIED.);
#24396=B_SPLINE_CURVE_WITH_KNOTS('',3,(#103957,#103958,#103959,#103960,
#103961,#103962,#103963,#103964,#103965),.UNSPECIFIED.,.F.,.F.,(4,1,1,1,
1,1,4),(10.3757270560178,11.2672252680712,12.2527713831816,13.2383174982921,
14.2238636134026,15.2094097285131,15.7079632679489),.UNSPECIFIED.);
#24397=B_SPLINE_CURVE_WITH_KNOTS('',3,(#103970,#103971,#103972,#103973,
#103974,#103975,#103976,#103977,#103978,#103979,#103980,#103981,#103982,
#103983,#103984,#103985,#103986,#103987,#103988,#103989,#103990,#103991,
#103992,#103993,#103994,#103995,#103996,#103997,#103998,#103999,#104000,
#104001,#104002,#104003,#104004,#104005,#104006,#104007,#104008,#104009,
#104010,#104011,#104012,#104013,#104014,#104015,#104016,#104017,#104018,
#104019,#104020,#104021,#104022,#104023,#104024,#104025,#104026,#104027,
#104028,#104029,#104030,#104031,#104032,#104033,#104034,#104035,#104036,
#104037,#104038,#104039,#104040,#104041,#104042,#104043,#104044,#104045,
#104046,#104047,#104048,#104049,#104050,#104051,#104052,#104053,#104054),
 .UNSPECIFIED.,.F.,.F.,(4,3,3,3,3,3,3,3,3,3,3,3,3,3,3,3,3,3,3,3,3,3,3,3,
3,3,3,3,4),(-0.36462930789068,-0.346303779262419,-0.324667498272067,-0.31532752509782,
-0.310804291325662,-0.289490474122718,-0.273816301221235,-0.265502639044791,
-0.261675347994805,-0.240939235060111,-0.220671177737736,-0.206527656031014,
-0.194625131687881,-0.19125128131443,-0.171660108944315,-0.164097090910849,
-0.143584954546993,-0.13429339168817,-0.128444126445644,-0.123952101242017,
-0.104508818706052,-0.0851257018425322,-0.0661288408609016,-0.0618227582712816,
-0.0586105122485322,-0.0400249876887114,-0.0217741310135354,-0.00410383987904057,
0.),.UNSPECIFIED.);
#24398=B_SPLINE_CURVE_WITH_KNOTS('',3,(#104058,#104059,#104060,#104061,
#104062,#104063,#104064,#104065),.UNSPECIFIED.,.F.,.F.,(4,1,1,1,1,4),(11.6154215191106,
12.6009676342211,13.5865137493315,14.572059864442,15.5576059795525,15.7079632679489),
 .UNSPECIFIED.);
#24399=B_SPLINE_CURVE_WITH_KNOTS('',3,(#104354,#104355,#104356,#104357,
#104358,#104359,#104360),.UNSPECIFIED.,.F.,.F.,(4,3,4),(-68.0026819426228,
-67.0171358275123,-66.9243948206342),.UNSPECIFIED.);
#29609=VERTEX_POINT('',#102630);
#29610=VERTEX_POINT('',#102631);
#29611=VERTEX_POINT('',#102633);
#29612=VERTEX_POINT('',#102644);
#29613=VERTEX_POINT('',#102654);
#29614=VERTEX_POINT('',#102655);
#29615=VERTEX_POINT('',#102702);
#29616=VERTEX_POINT('',#102703);
#29617=VERTEX_POINT('',#102750);
#29618=VERTEX_POINT('',#102751);
#29619=VERTEX_POINT('',#102804);
#29620=VERTEX_POINT('',#102805);
#29621=VERTEX_POINT('',#102852);
#29622=VERTEX_POINT('',#102853);
#29623=VERTEX_POINT('',#102906);
#29624=VERTEX_POINT('',#102907);
#29625=VERTEX_POINT('',#102954);
#29626=VERTEX_POINT('',#102955);
#29627=VERTEX_POINT('',#103002);
#29628=VERTEX_POINT('',#103003);
#29629=VERTEX_POINT('',#103056);
#29630=VERTEX_POINT('',#103057);
#29631=VERTEX_POINT('',#103104);
#29632=VERTEX_POINT('',#103105);
#29633=VERTEX_POINT('',#103152);
#29634=VERTEX_POINT('',#103153);
#29635=VERTEX_POINT('',#103155);
#29636=VERTEX_POINT('',#103165);
#29637=VERTEX_POINT('',#103176);
#29638=VERTEX_POINT('',#103177);
#29639=VERTEX_POINT('',#103200);
#29640=VERTEX_POINT('',#103201);
#29641=VERTEX_POINT('',#103225);
#29642=VERTEX_POINT('',#103226);
#29643=VERTEX_POINT('',#103250);
#29644=VERTEX_POINT('',#103251);
#29645=VERTEX_POINT('',#103274);
#29646=VERTEX_POINT('',#103275);
#29647=VERTEX_POINT('',#103299);
#29648=VERTEX_POINT('',#103300);
#29649=VERTEX_POINT('',#103324);
#29650=VERTEX_POINT('',#103325);
#29651=VERTEX_POINT('',#103349);
#29652=VERTEX_POINT('',#103350);
#29653=VERTEX_POINT('',#103374);
#29654=VERTEX_POINT('',#103375);
#29655=VERTEX_POINT('',#103398);
#29656=VERTEX_POINT('',#103484);
#29657=VERTEX_POINT('',#103486);
#29658=VERTEX_POINT('',#103871);
#29659=VERTEX_POINT('',#103967);
#29660=VERTEX_POINT('',#103969);
#29661=VERTEX_POINT('',#104362);
#29662=VERTEX_POINT('',#104366);
#29663=VERTEX_POINT('',#104371);
#29664=VERTEX_POINT('',#104372);
#29665=VERTEX_POINT('',#104374);
#29666=VERTEX_POINT('',#104376);
#29667=VERTEX_POINT('',#104378);
#29668=VERTEX_POINT('',#104382);
#29669=VERTEX_POINT('',#104388);
#29670=VERTEX_POINT('',#104389);
#29671=VERTEX_POINT('',#104391);
#29672=VERTEX_POINT('',#104395);
#29673=VERTEX_POINT('',#104397);
#29674=VERTEX_POINT('',#104401);
#29675=VERTEX_POINT('',#104406);
#29676=VERTEX_POINT('',#104420);
#37878=EDGE_CURVE('',#29609,#29610,#16416,.T.);
#37879=EDGE_CURVE('',#29609,#29611,#24350,.T.);
#37880=EDGE_CURVE('',#29612,#29611,#1284,.T.);
#37881=EDGE_CURVE('',#29612,#29610,#24351,.T.);
#37882=EDGE_CURVE('',#29613,#29614,#16417,.T.);
#37883=EDGE_CURVE('',#29613,#29609,#24352,.T.);
#37884=EDGE_CURVE('',#29610,#29614,#24353,.T.);
#37885=EDGE_CURVE('',#29615,#29616,#16418,.T.);
#37886=EDGE_CURVE('',#29615,#29613,#24354,.T.);
#37887=EDGE_CURVE('',#29614,#29616,#24355,.T.);
#37888=EDGE_CURVE('',#29617,#29618,#16419,.T.);
#37889=EDGE_CURVE('',#29617,#29615,#24356,.T.);
#37890=EDGE_CURVE('',#29616,#29618,#24357,.T.);
#37891=EDGE_CURVE('',#29619,#29620,#16420,.T.);
#37892=EDGE_CURVE('',#29619,#29617,#24358,.T.);
#37893=EDGE_CURVE('',#29618,#29620,#24359,.T.);
#37894=EDGE_CURVE('',#29621,#29622,#16421,.T.);
#37895=EDGE_CURVE('',#29621,#29619,#24360,.T.);
#37896=EDGE_CURVE('',#29620,#29622,#24361,.T.);
#37897=EDGE_CURVE('',#29623,#29624,#16422,.T.);
#37898=EDGE_CURVE('',#29623,#29621,#24362,.T.);
#37899=EDGE_CURVE('',#29622,#29624,#24363,.T.);
#37900=EDGE_CURVE('',#29625,#29626,#16423,.T.);
#37901=EDGE_CURVE('',#29625,#29623,#24364,.T.);
#37902=EDGE_CURVE('',#29624,#29626,#24365,.T.);
#37903=EDGE_CURVE('',#29627,#29628,#16424,.T.);
#37904=EDGE_CURVE('',#29627,#29625,#24366,.T.);
#37905=EDGE_CURVE('',#29626,#29628,#24367,.T.);
#37906=EDGE_CURVE('',#29629,#29630,#16425,.T.);
#37907=EDGE_CURVE('',#29629,#29627,#24368,.T.);
#37908=EDGE_CURVE('',#29628,#29630,#24369,.T.);
#37909=EDGE_CURVE('',#29631,#29632,#16426,.T.);
#37910=EDGE_CURVE('',#29631,#29629,#24370,.T.);
#37911=EDGE_CURVE('',#29630,#29632,#24371,.T.);
#37912=EDGE_CURVE('',#29633,#29634,#16427,.T.);
#37913=EDGE_CURVE('',#29633,#29635,#24372,.T.);
#37914=EDGE_CURVE('',#29636,#29635,#1285,.T.);
#37915=EDGE_CURVE('',#29634,#29636,#24373,.T.);
#37916=EDGE_CURVE('',#29637,#29638,#16428,.T.);
#37917=EDGE_CURVE('',#29637,#29633,#24374,.T.);
#37918=EDGE_CURVE('',#29638,#29634,#24375,.T.);
#37919=EDGE_CURVE('',#29639,#29640,#16429,.T.);
#37920=EDGE_CURVE('',#29639,#29637,#24376,.T.);
#37921=EDGE_CURVE('',#29640,#29638,#24377,.T.);
#37922=EDGE_CURVE('',#29641,#29642,#16430,.T.);
#37923=EDGE_CURVE('',#29641,#29639,#24378,.T.);
#37924=EDGE_CURVE('',#29642,#29640,#24379,.T.);
#37925=EDGE_CURVE('',#29643,#29644,#16431,.T.);
#37926=EDGE_CURVE('',#29643,#29641,#24380,.T.);
#37927=EDGE_CURVE('',#29644,#29642,#24381,.T.);
#37928=EDGE_CURVE('',#29645,#29646,#16432,.T.);
#37929=EDGE_CURVE('',#29645,#29643,#24382,.T.);
#37930=EDGE_CURVE('',#29646,#29644,#24383,.T.);
#37931=EDGE_CURVE('',#29647,#29648,#16433,.T.);
#37932=EDGE_CURVE('',#29647,#29645,#24384,.T.);
#37933=EDGE_CURVE('',#29648,#29646,#24385,.T.);
#37934=EDGE_CURVE('',#29649,#29650,#16434,.T.);
#37935=EDGE_CURVE('',#29649,#29647,#24386,.T.);
#37936=EDGE_CURVE('',#29650,#29648,#24387,.T.);
#37937=EDGE_CURVE('',#29651,#29652,#16435,.T.);
#37938=EDGE_CURVE('',#29651,#29649,#24388,.T.);
#37939=EDGE_CURVE('',#29652,#29650,#24389,.T.);
#37940=EDGE_CURVE('',#29653,#29654,#16436,.T.);
#37941=EDGE_CURVE('',#29653,#29651,#24390,.T.);
#37942=EDGE_CURVE('',#29654,#29652,#24391,.T.);
#37943=EDGE_CURVE('',#29635,#29655,#24392,.T.);
#37944=EDGE_CURVE('',#29656,#29655,#1286,.F.);
#37945=EDGE_CURVE('',#29657,#29656,#1287,.F.);
#37946=EDGE_CURVE('',#29657,#29636,#24393,.T.);
#37947=EDGE_CURVE('',#29632,#29657,#24394,.T.);
#37948=EDGE_CURVE('',#29658,#29612,#24395,.T.);
#37949=EDGE_CURVE('',#29658,#29654,#24396,.T.);
#37950=EDGE_CURVE('',#29611,#29659,#1288,.T.);
#37951=EDGE_CURVE('',#29611,#29660,#24397,.T.);
#37952=EDGE_CURVE('',#29660,#29658,#1289,.T.);
#37953=EDGE_CURVE('',#29659,#29612,#1290,.T.);
#37954=EDGE_CURVE('',#29660,#29653,#24398,.T.);
#37955=EDGE_CURVE('',#29655,#29631,#24399,.T.);
#37956=EDGE_CURVE('',#29661,#29661,#1291,.T.);
#37957=EDGE_CURVE('',#29661,#29659,#1292,.T.);
#37958=EDGE_CURVE('',#29662,#29662,#1293,.T.);
#37959=EDGE_CURVE('',#29655,#29657,#1294,.F.);
#37960=EDGE_CURVE('',#29663,#29664,#16437,.T.);
#37961=EDGE_CURVE('',#29663,#29665,#16438,.T.);
#37962=EDGE_CURVE('',#29666,#29665,#16439,.T.);
#37963=EDGE_CURVE('',#29667,#29666,#379,.T.);
#37964=EDGE_CURVE('',#29668,#29667,#16440,.T.);
#37965=EDGE_CURVE('',#29664,#29668,#380,.T.);
#37966=EDGE_CURVE('',#29669,#29670,#16441,.T.);
#37967=EDGE_CURVE('',#29671,#29669,#381,.T.);
#37968=EDGE_CURVE('',#29672,#29671,#16442,.T.);
#37969=EDGE_CURVE('',#29673,#29672,#382,.T.);
#37970=EDGE_CURVE('',#29674,#29673,#16443,.T.);
#37971=EDGE_CURVE('',#29674,#29670,#16444,.T.);
#37972=EDGE_CURVE('',#29670,#29663,#1295,.T.);
#37973=EDGE_CURVE('',#29675,#29674,#1296,.T.);
#37974=EDGE_CURVE('',#29665,#29675,#1297,.T.);
#37975=EDGE_CURVE('',#29673,#29669,#1298,.T.);
#37976=EDGE_CURVE('',#29672,#29671,#1299,.T.);
#37977=EDGE_CURVE('',#29668,#29667,#1300,.T.);
#37978=EDGE_CURVE('',#29664,#29666,#1301,.T.);
#37979=EDGE_CURVE('',#29662,#29675,#16445,.T.);
#37980=EDGE_CURVE('',#29676,#29676,#1302,.T.);
#37981=EDGE_CURVE('',#29676,#29656,#16446,.T.);
#54091=ORIENTED_EDGE('',*,*,#37878,.F.);
#54092=ORIENTED_EDGE('',*,*,#37879,.T.);
#54093=ORIENTED_EDGE('',*,*,#37880,.F.);
#54094=ORIENTED_EDGE('',*,*,#37881,.T.);
#54095=ORIENTED_EDGE('',*,*,#37882,.F.);
#54096=ORIENTED_EDGE('',*,*,#37883,.T.);
#54097=ORIENTED_EDGE('',*,*,#37878,.T.);
#54098=ORIENTED_EDGE('',*,*,#37884,.T.);
#54099=ORIENTED_EDGE('',*,*,#37885,.F.);
#54100=ORIENTED_EDGE('',*,*,#37886,.T.);
#54101=ORIENTED_EDGE('',*,*,#37882,.T.);
#54102=ORIENTED_EDGE('',*,*,#37887,.T.);
#54103=ORIENTED_EDGE('',*,*,#37888,.F.);
#54104=ORIENTED_EDGE('',*,*,#37889,.T.);
#54105=ORIENTED_EDGE('',*,*,#37885,.T.);
#54106=ORIENTED_EDGE('',*,*,#37890,.T.);
#54107=ORIENTED_EDGE('',*,*,#37891,.F.);
#54108=ORIENTED_EDGE('',*,*,#37892,.T.);
#54109=ORIENTED_EDGE('',*,*,#37888,.T.);
#54110=ORIENTED_EDGE('',*,*,#37893,.T.);
#54111=ORIENTED_EDGE('',*,*,#37894,.F.);
#54112=ORIENTED_EDGE('',*,*,#37895,.T.);
#54113=ORIENTED_EDGE('',*,*,#37891,.T.);
#54114=ORIENTED_EDGE('',*,*,#37896,.T.);
#54115=ORIENTED_EDGE('',*,*,#37897,.F.);
#54116=ORIENTED_EDGE('',*,*,#37898,.T.);
#54117=ORIENTED_EDGE('',*,*,#37894,.T.);
#54118=ORIENTED_EDGE('',*,*,#37899,.T.);
#54119=ORIENTED_EDGE('',*,*,#37900,.F.);
#54120=ORIENTED_EDGE('',*,*,#37901,.T.);
#54121=ORIENTED_EDGE('',*,*,#37897,.T.);
#54122=ORIENTED_EDGE('',*,*,#37902,.T.);
#54123=ORIENTED_EDGE('',*,*,#37903,.F.);
#54124=ORIENTED_EDGE('',*,*,#37904,.T.);
#54125=ORIENTED_EDGE('',*,*,#37900,.T.);
#54126=ORIENTED_EDGE('',*,*,#37905,.T.);
#54127=ORIENTED_EDGE('',*,*,#37906,.F.);
#54128=ORIENTED_EDGE('',*,*,#37907,.T.);
#54129=ORIENTED_EDGE('',*,*,#37903,.T.);
#54130=ORIENTED_EDGE('',*,*,#37908,.T.);
#54131=ORIENTED_EDGE('',*,*,#37909,.F.);
#54132=ORIENTED_EDGE('',*,*,#37910,.T.);
#54133=ORIENTED_EDGE('',*,*,#37906,.T.);
#54134=ORIENTED_EDGE('',*,*,#37911,.T.);
#54135=ORIENTED_EDGE('',*,*,#37912,.F.);
#54136=ORIENTED_EDGE('',*,*,#37913,.T.);
#54137=ORIENTED_EDGE('',*,*,#37914,.F.);
#54138=ORIENTED_EDGE('',*,*,#37915,.F.);
#54139=ORIENTED_EDGE('',*,*,#37916,.F.);
#54140=ORIENTED_EDGE('',*,*,#37917,.T.);
#54141=ORIENTED_EDGE('',*,*,#37912,.T.);
#54142=ORIENTED_EDGE('',*,*,#37918,.F.);
#54143=ORIENTED_EDGE('',*,*,#37919,.F.);
#54144=ORIENTED_EDGE('',*,*,#37920,.T.);
#54145=ORIENTED_EDGE('',*,*,#37916,.T.);
#54146=ORIENTED_EDGE('',*,*,#37921,.F.);
#54147=ORIENTED_EDGE('',*,*,#37922,.F.);
#54148=ORIENTED_EDGE('',*,*,#37923,.T.);
#54149=ORIENTED_EDGE('',*,*,#37919,.T.);
#54150=ORIENTED_EDGE('',*,*,#37924,.F.);
#54151=ORIENTED_EDGE('',*,*,#37925,.F.);
#54152=ORIENTED_EDGE('',*,*,#37926,.T.);
#54153=ORIENTED_EDGE('',*,*,#37922,.T.);
#54154=ORIENTED_EDGE('',*,*,#37927,.F.);
#54155=ORIENTED_EDGE('',*,*,#37928,.F.);
#54156=ORIENTED_EDGE('',*,*,#37929,.T.);
#54157=ORIENTED_EDGE('',*,*,#37925,.T.);
#54158=ORIENTED_EDGE('',*,*,#37930,.F.);
#54159=ORIENTED_EDGE('',*,*,#37931,.F.);
#54160=ORIENTED_EDGE('',*,*,#37932,.T.);
#54161=ORIENTED_EDGE('',*,*,#37928,.T.);
#54162=ORIENTED_EDGE('',*,*,#37933,.F.);
#54163=ORIENTED_EDGE('',*,*,#37934,.F.);
#54164=ORIENTED_EDGE('',*,*,#37935,.T.);
#54165=ORIENTED_EDGE('',*,*,#37931,.T.);
#54166=ORIENTED_EDGE('',*,*,#37936,.F.);
#54167=ORIENTED_EDGE('',*,*,#37937,.F.);
#54168=ORIENTED_EDGE('',*,*,#37938,.T.);
#54169=ORIENTED_EDGE('',*,*,#37934,.T.);
#54170=ORIENTED_EDGE('',*,*,#37939,.F.);
#54171=ORIENTED_EDGE('',*,*,#37940,.F.);
#54172=ORIENTED_EDGE('',*,*,#37941,.T.);
#54173=ORIENTED_EDGE('',*,*,#37937,.T.);
#54174=ORIENTED_EDGE('',*,*,#37942,.F.);
#54175=ORIENTED_EDGE('',*,*,#37914,.T.);
#54176=ORIENTED_EDGE('',*,*,#37943,.T.);
#54177=ORIENTED_EDGE('',*,*,#37944,.F.);
#54178=ORIENTED_EDGE('',*,*,#37945,.F.);
#54179=ORIENTED_EDGE('',*,*,#37946,.T.);
#54180=ORIENTED_EDGE('',*,*,#37946,.F.);
#54181=ORIENTED_EDGE('',*,*,#37947,.F.);
#54182=ORIENTED_EDGE('',*,*,#37911,.F.);
#54183=ORIENTED_EDGE('',*,*,#37908,.F.);
#54184=ORIENTED_EDGE('',*,*,#37905,.F.);
#54185=ORIENTED_EDGE('',*,*,#37902,.F.);
#54186=ORIENTED_EDGE('',*,*,#37899,.F.);
#54187=ORIENTED_EDGE('',*,*,#37896,.F.);
#54188=ORIENTED_EDGE('',*,*,#37893,.F.);
#54189=ORIENTED_EDGE('',*,*,#37890,.F.);
#54190=ORIENTED_EDGE('',*,*,#37887,.F.);
#54191=ORIENTED_EDGE('',*,*,#37884,.F.);
#54192=ORIENTED_EDGE('',*,*,#37881,.F.);
#54193=ORIENTED_EDGE('',*,*,#37948,.F.);
#54194=ORIENTED_EDGE('',*,*,#37949,.T.);
#54195=ORIENTED_EDGE('',*,*,#37942,.T.);
#54196=ORIENTED_EDGE('',*,*,#37939,.T.);
#54197=ORIENTED_EDGE('',*,*,#37936,.T.);
#54198=ORIENTED_EDGE('',*,*,#37933,.T.);
#54199=ORIENTED_EDGE('',*,*,#37930,.T.);
#54200=ORIENTED_EDGE('',*,*,#37927,.T.);
#54201=ORIENTED_EDGE('',*,*,#37924,.T.);
#54202=ORIENTED_EDGE('',*,*,#37921,.T.);
#54203=ORIENTED_EDGE('',*,*,#37918,.T.);
#54204=ORIENTED_EDGE('',*,*,#37915,.T.);
#54205=ORIENTED_EDGE('',*,*,#37950,.F.);
#54206=ORIENTED_EDGE('',*,*,#37951,.T.);
#54207=ORIENTED_EDGE('',*,*,#37952,.T.);
#54208=ORIENTED_EDGE('',*,*,#37948,.T.);
#54209=ORIENTED_EDGE('',*,*,#37953,.F.);
#54210=ORIENTED_EDGE('',*,*,#37940,.T.);
#54211=ORIENTED_EDGE('',*,*,#37949,.F.);
#54212=ORIENTED_EDGE('',*,*,#37952,.F.);
#54213=ORIENTED_EDGE('',*,*,#37954,.T.);
#54214=ORIENTED_EDGE('',*,*,#37943,.F.);
#54215=ORIENTED_EDGE('',*,*,#37913,.F.);
#54216=ORIENTED_EDGE('',*,*,#37917,.F.);
#54217=ORIENTED_EDGE('',*,*,#37920,.F.);
#54218=ORIENTED_EDGE('',*,*,#37923,.F.);
#54219=ORIENTED_EDGE('',*,*,#37926,.F.);
#54220=ORIENTED_EDGE('',*,*,#37929,.F.);
#54221=ORIENTED_EDGE('',*,*,#37932,.F.);
#54222=ORIENTED_EDGE('',*,*,#37935,.F.);
#54223=ORIENTED_EDGE('',*,*,#37938,.F.);
#54224=ORIENTED_EDGE('',*,*,#37941,.F.);
#54225=ORIENTED_EDGE('',*,*,#37954,.F.);
#54226=ORIENTED_EDGE('',*,*,#37951,.F.);
#54227=ORIENTED_EDGE('',*,*,#37879,.F.);
#54228=ORIENTED_EDGE('',*,*,#37883,.F.);
#54229=ORIENTED_EDGE('',*,*,#37886,.F.);
#54230=ORIENTED_EDGE('',*,*,#37889,.F.);
#54231=ORIENTED_EDGE('',*,*,#37892,.F.);
#54232=ORIENTED_EDGE('',*,*,#37895,.F.);
#54233=ORIENTED_EDGE('',*,*,#37898,.F.);
#54234=ORIENTED_EDGE('',*,*,#37901,.F.);
#54235=ORIENTED_EDGE('',*,*,#37904,.F.);
#54236=ORIENTED_EDGE('',*,*,#37907,.F.);
#54237=ORIENTED_EDGE('',*,*,#37910,.F.);
#54238=ORIENTED_EDGE('',*,*,#37955,.F.);
#54239=ORIENTED_EDGE('',*,*,#37956,.T.);
#54240=ORIENTED_EDGE('',*,*,#37957,.T.);
#54241=ORIENTED_EDGE('',*,*,#37953,.T.);
#54242=ORIENTED_EDGE('',*,*,#37880,.T.);
#54243=ORIENTED_EDGE('',*,*,#37950,.T.);
#54244=ORIENTED_EDGE('',*,*,#37957,.F.);
#54245=ORIENTED_EDGE('',*,*,#37958,.T.);
#54246=ORIENTED_EDGE('',*,*,#37956,.F.);
#54247=ORIENTED_EDGE('',*,*,#37909,.T.);
#54248=ORIENTED_EDGE('',*,*,#37947,.T.);
#54249=ORIENTED_EDGE('',*,*,#37959,.F.);
#54250=ORIENTED_EDGE('',*,*,#37955,.T.);
#54251=ORIENTED_EDGE('',*,*,#37960,.F.);
#54252=ORIENTED_EDGE('',*,*,#37961,.T.);
#54253=ORIENTED_EDGE('',*,*,#37962,.F.);
#54254=ORIENTED_EDGE('',*,*,#37963,.F.);
#54255=ORIENTED_EDGE('',*,*,#37964,.F.);
#54256=ORIENTED_EDGE('',*,*,#37965,.F.);
#54257=ORIENTED_EDGE('',*,*,#37966,.F.);
#54258=ORIENTED_EDGE('',*,*,#37967,.F.);
#54259=ORIENTED_EDGE('',*,*,#37968,.F.);
#54260=ORIENTED_EDGE('',*,*,#37969,.F.);
#54261=ORIENTED_EDGE('',*,*,#37970,.F.);
#54262=ORIENTED_EDGE('',*,*,#37971,.T.);
#54263=ORIENTED_EDGE('',*,*,#37972,.F.);
#54264=ORIENTED_EDGE('',*,*,#37971,.F.);
#54265=ORIENTED_EDGE('',*,*,#37973,.F.);
#54266=ORIENTED_EDGE('',*,*,#37974,.F.);
#54267=ORIENTED_EDGE('',*,*,#37961,.F.);
#54268=ORIENTED_EDGE('',*,*,#37967,.T.);
#54269=ORIENTED_EDGE('',*,*,#37975,.F.);
#54270=ORIENTED_EDGE('',*,*,#37969,.T.);
#54271=ORIENTED_EDGE('',*,*,#37976,.T.);
#54272=ORIENTED_EDGE('',*,*,#37965,.T.);
#54273=ORIENTED_EDGE('',*,*,#37977,.T.);
#54274=ORIENTED_EDGE('',*,*,#37963,.T.);
#54275=ORIENTED_EDGE('',*,*,#37978,.F.);
#54276=ORIENTED_EDGE('',*,*,#37968,.T.);
#54277=ORIENTED_EDGE('',*,*,#37976,.F.);
#54278=ORIENTED_EDGE('',*,*,#37964,.T.);
#54279=ORIENTED_EDGE('',*,*,#37977,.F.);
#54280=ORIENTED_EDGE('',*,*,#37958,.F.);
#54281=ORIENTED_EDGE('',*,*,#37979,.T.);
#54282=ORIENTED_EDGE('',*,*,#37973,.T.);
#54283=ORIENTED_EDGE('',*,*,#37970,.T.);
#54284=ORIENTED_EDGE('',*,*,#37975,.T.);
#54285=ORIENTED_EDGE('',*,*,#37966,.T.);
#54286=ORIENTED_EDGE('',*,*,#37972,.T.);
#54287=ORIENTED_EDGE('',*,*,#37960,.T.);
#54288=ORIENTED_EDGE('',*,*,#37978,.T.);
#54289=ORIENTED_EDGE('',*,*,#37962,.T.);
#54290=ORIENTED_EDGE('',*,*,#37974,.T.);
#54291=ORIENTED_EDGE('',*,*,#37979,.F.);
#54292=ORIENTED_EDGE('',*,*,#37980,.F.);
#54293=ORIENTED_EDGE('',*,*,#37981,.T.);
#54294=ORIENTED_EDGE('',*,*,#37944,.T.);
#54295=ORIENTED_EDGE('',*,*,#37959,.T.);
#54296=ORIENTED_EDGE('',*,*,#37945,.T.);
#54297=ORIENTED_EDGE('',*,*,#37981,.F.);
#54298=ORIENTED_EDGE('',*,*,#37980,.T.);
#57111=B_SPLINE_SURFACE_WITH_KNOTS('',3,3,((#103573,#103574,#103575,#103576,
#103577,#103578,#103579,#103580,#103581,#103582,#103583,#103584,#103585,
#103586,#103587,#103588,#103589,#103590,#103591,#103592,#103593,#103594,
#103595,#103596,#103597,#103598,#103599,#103600,#103601,#103602,#103603,
#103604,#103605,#103606,#103607,#103608,#103609,#103610,#103611,#103612,
#103613,#103614,#103615,#103616,#103617,#103618,#103619,#103620,#103621,
#103622,#103623,#103624,#103625,#103626,#103627,#103628,#103629,#103630,
#103631,#103632,#103633,#103634,#103635,#103636,#103637,#103638,#103639,
#103640,#103641,#103642,#103643,#103644),(#103645,#103646,#103647,#103648,
#103649,#103650,#103651,#103652,#103653,#103654,#103655,#103656,#103657,
#103658,#103659,#103660,#103661,#103662,#103663,#103664,#103665,#103666,
#103667,#103668,#103669,#103670,#103671,#103672,#103673,#103674,#103675,
#103676,#103677,#103678,#103679,#103680,#103681,#103682,#103683,#103684,
#103685,#103686,#103687,#103688,#103689,#103690,#103691,#103692,#103693,
#103694,#103695,#103696,#103697,#103698,#103699,#103700,#103701,#103702,
#103703,#103704,#103705,#103706,#103707,#103708,#103709,#103710,#103711,
#103712,#103713,#103714,#103715,#103716),(#103717,#103718,#103719,#103720,
#103721,#103722,#103723,#103724,#103725,#103726,#103727,#103728,#103729,
#103730,#103731,#103732,#103733,#103734,#103735,#103736,#103737,#103738,
#103739,#103740,#103741,#103742,#103743,#103744,#103745,#103746,#103747,
#103748,#103749,#103750,#103751,#103752,#103753,#103754,#103755,#103756,
#103757,#103758,#103759,#103760,#103761,#103762,#103763,#103764,#103765,
#103766,#103767,#103768,#103769,#103770,#103771,#103772,#103773,#103774,
#103775,#103776,#103777,#103778,#103779,#103780,#103781,#103782,#103783,
#103784,#103785,#103786,#103787,#103788),(#103789,#103790,#103791,#103792,
#103793,#103794,#103795,#103796,#103797,#103798,#103799,#103800,#103801,
#103802,#103803,#103804,#103805,#103806,#103807,#103808,#103809,#103810,
#103811,#103812,#103813,#103814,#103815,#103816,#103817,#103818,#103819,
#103820,#103821,#103822,#103823,#103824,#103825,#103826,#103827,#103828,
#103829,#103830,#103831,#103832,#103833,#103834,#103835,#103836,#103837,
#103838,#103839,#103840,#103841,#103842,#103843,#103844,#103845,#103846,
#103847,#103848,#103849,#103850,#103851,#103852,#103853,#103854,#103855,
#103856,#103857,#103858,#103859,#103860)),.UNSPECIFIED.,.F.,.F.,.F.,(4,
4),(4,1,1,1,1,1,1,1,1,1,1,1,1,1,1,1,1,1,1,1,1,1,1,1,1,1,1,1,1,1,1,1,1,1,
1,1,1,1,1,1,1,1,1,1,1,1,1,1,1,1,1,1,1,1,1,1,1,1,1,1,1,1,1,1,1,1,1,1,1,4),
(0.,0.0460148164544127),(8.31058692273973,9.29613303785021,10.2816791529607,
11.2672252680712,12.2527713831816,13.2383174982921,14.2238636134026,15.2094097285131,
16.1949558436235,17.180501958734,18.1660480738445,19.151594188955,20.1371403040654,
21.1226864191759,22.1082325342864,23.0937786493969,24.0793247645073,25.0648708796178,
26.0504169947283,27.0359631098388,28.0215092249492,29.0070553400597,29.9926014551702,
30.9781475702807,31.9636936853911,32.9492398005016,33.9347859156121,34.9203320307226,
35.905878145833,36.8914242609435,37.876970376054,38.8625164911645,39.8480626062749,
40.8336087213854,41.8191548364959,42.8047009516064,43.7902470667168,44.7757931818273,
45.7613392969378,46.7468854120483,47.7324315271587,48.7179776422692,49.7035237573797,
50.6890698724902,51.6746159876006,52.6601621027111,53.6457082178216,54.6312543329321,
55.6168004480425,56.602346563153,57.5878926782635,58.573438793374,59.5589849084844,
60.5445310235949,61.5300771387054,62.5156232538159,63.5011693689263,64.4867154840368,
65.4722615991473,66.4578077142578,67.4433538293682,68.4288999444787,69.4144460595892,
70.3999921746997,71.3855382898101,72.3710844049206,73.3566305200311,74.3421766351416,
75.327722750252,76.3132688653625),.UNSPECIFIED.);
#57112=B_SPLINE_SURFACE_WITH_KNOTS('',3,3,((#104066,#104067,#104068,#104069,
#104070,#104071,#104072,#104073,#104074,#104075,#104076,#104077,#104078,
#104079,#104080,#104081,#104082,#104083,#104084,#104085,#104086,#104087,
#104088,#104089,#104090,#104091,#104092,#104093,#104094,#104095,#104096,
#104097,#104098,#104099,#104100,#104101,#104102,#104103,#104104,#104105,
#104106,#104107,#104108,#104109,#104110,#104111,#104112,#104113,#104114,
#104115,#104116,#104117,#104118,#104119,#104120,#104121,#104122,#104123,
#104124,#104125,#104126,#104127,#104128,#104129,#104130,#104131,#104132,
#104133,#104134,#104135,#104136,#104137),(#104138,#104139,#104140,#104141,
#104142,#104143,#104144,#104145,#104146,#104147,#104148,#104149,#104150,
#104151,#104152,#104153,#104154,#104155,#104156,#104157,#104158,#104159,
#104160,#104161,#104162,#104163,#104164,#104165,#104166,#104167,#104168,
#104169,#104170,#104171,#104172,#104173,#104174,#104175,#104176,#104177,
#104178,#104179,#104180,#104181,#104182,#104183,#104184,#104185,#104186,
#104187,#104188,#104189,#104190,#104191,#104192,#104193,#104194,#104195,
#104196,#104197,#104198,#104199,#104200,#104201,#104202,#104203,#104204,
#104205,#104206,#104207,#104208,#104209),(#104210,#104211,#104212,#104213,
#104214,#104215,#104216,#104217,#104218,#104219,#104220,#104221,#104222,
#104223,#104224,#104225,#104226,#104227,#104228,#104229,#104230,#104231,
#104232,#104233,#104234,#104235,#104236,#104237,#104238,#104239,#104240,
#104241,#104242,#104243,#104244,#104245,#104246,#104247,#104248,#104249,
#104250,#104251,#104252,#104253,#104254,#104255,#104256,#104257,#104258,
#104259,#104260,#104261,#104262,#104263,#104264,#104265,#104266,#104267,
#104268,#104269,#104270,#104271,#104272,#104273,#104274,#104275,#104276,
#104277,#104278,#104279,#104280,#104281),(#104282,#104283,#104284,#104285,
#104286,#104287,#104288,#104289,#104290,#104291,#104292,#104293,#104294,
#104295,#104296,#104297,#104298,#104299,#104300,#104301,#104302,#104303,
#104304,#104305,#104306,#104307,#104308,#104309,#104310,#104311,#104312,
#104313,#104314,#104315,#104316,#104317,#104318,#104319,#104320,#104321,
#104322,#104323,#104324,#104325,#104326,#104327,#104328,#104329,#104330,
#104331,#104332,#104333,#104334,#104335,#104336,#104337,#104338,#104339,
#104340,#104341,#104342,#104343,#104344,#104345,#104346,#104347,#104348,
#104349,#104350,#104351,#104352,#104353)),.UNSPECIFIED.,.F.,.F.,.F.,(4,
4),(4,1,1,1,1,1,1,1,1,1,1,1,1,1,1,1,1,1,1,1,1,1,1,1,1,1,1,1,1,1,1,1,1,1,
1,1,1,1,1,1,1,1,1,1,1,1,1,1,1,1,1,1,1,1,1,1,1,1,1,1,1,1,1,1,1,1,1,1,1,4),
(0.,0.0460148164544127),(11.6154215191106,12.6009676342211,13.5865137493315,
14.572059864442,15.5576059795525,16.543152094663,17.5286982097734,18.5142443248839,
19.4997904399944,20.4853365551049,21.4708826702153,22.4564287853258,23.4419749004363,
24.4275210155468,25.4130671306572,26.3986132457677,27.3841593608782,28.3697054759887,
29.3552515910991,30.3407977062096,31.3263438213201,32.3118899364306,33.297436051541,
34.2829821666515,35.268528281762,36.2540743968725,37.2396205119829,38.2251666270934,
39.2107127422039,40.1962588573144,41.1818049724248,42.1673510875353,43.1528972026458,
44.1384433177563,45.1239894328667,46.1095355479772,47.0950816630877,48.0806277781982,
49.0661738933086,50.0517200084191,51.0372661235296,52.0228122386401,53.0083583537505,
53.993904468861,54.9794505839715,55.964996699082,56.9505428141924,57.9360889293029,
58.9216350444134,59.9071811595239,60.8927272746343,61.8782733897448,62.8638195048553,
63.8493656199658,64.8349117350762,65.8204578501867,66.8060039652972,67.7915500804077,
68.7770961955181,69.7626423106286,70.7481884257391,71.7337345408496,72.71928065596,
73.7048267710705,74.690372886181,75.6759190012915,76.6614651164019,77.6470112315124,
78.6325573466229,79.6181034617334),.UNSPECIFIED.);
#59950=ADVANCED_FACE('',(#6850),#718,.T.);
#59951=ADVANCED_FACE('',(#6851),#719,.T.);
#59952=ADVANCED_FACE('',(#6852),#720,.T.);
#59953=ADVANCED_FACE('',(#6853),#721,.T.);
#59954=ADVANCED_FACE('',(#6854),#722,.T.);
#59955=ADVANCED_FACE('',(#6855),#723,.T.);
#59956=ADVANCED_FACE('',(#6856),#724,.T.);
#59957=ADVANCED_FACE('',(#6857),#725,.T.);
#59958=ADVANCED_FACE('',(#6858),#726,.T.);
#59959=ADVANCED_FACE('',(#6859),#727,.T.);
#59960=ADVANCED_FACE('',(#6860),#728,.T.);
#59961=ADVANCED_FACE('',(#6861),#729,.T.);
#59962=ADVANCED_FACE('',(#6862),#730,.T.);
#59963=ADVANCED_FACE('',(#6863),#731,.T.);
#59964=ADVANCED_FACE('',(#6864),#732,.T.);
#59965=ADVANCED_FACE('',(#6865),#733,.T.);
#59966=ADVANCED_FACE('',(#6866),#734,.T.);
#59967=ADVANCED_FACE('',(#6867),#735,.T.);
#59968=ADVANCED_FACE('',(#6868),#736,.T.);
#59969=ADVANCED_FACE('',(#6869),#737,.T.);
#59970=ADVANCED_FACE('',(#6870),#738,.T.);
#59971=ADVANCED_FACE('',(#6871),#3784,.F.);
#59972=ADVANCED_FACE('',(#6872),#57111,.F.);
#59973=ADVANCED_FACE('',(#6873),#3785,.T.);
#59974=ADVANCED_FACE('',(#6874),#739,.T.);
#59975=ADVANCED_FACE('',(#6875),#57112,.F.);
#59976=ADVANCED_FACE('',(#6876),#107,.F.);
#59977=ADVANCED_FACE('',(#6877,#1851),#3786,.T.);
#59978=ADVANCED_FACE('',(#6878),#740,.T.);
#59979=ADVANCED_FACE('',(#6879),#3787,.F.);
#59980=ADVANCED_FACE('',(#6880),#3788,.F.);
#59981=ADVANCED_FACE('',(#6881),#3789,.F.);
#59982=ADVANCED_FACE('',(#6882),#930,.T.);
#59983=ADVANCED_FACE('',(#6883),#931,.T.);
#59984=ADVANCED_FACE('',(#6884),#3790,.T.);
#59985=ADVANCED_FACE('',(#6885),#3791,.T.);
#59986=ADVANCED_FACE('',(#6886),#741,.T.);
#59987=ADVANCED_FACE('',(#6887),#932,.T.);
#59988=ADVANCED_FACE('',(#6888),#3792,.T.);
#60402=CLOSED_SHELL('',(#59950,#59951,#59952,#59953,#59954,#59955,#59956,
#59957,#59958,#59959,#59960,#59961,#59962,#59963,#59964,#59965,#59966,#59967,
#59968,#59969,#59970,#59971,#59972,#59973,#59974,#59975,#59976,#59977,#59978,
#59979,#59980,#59981,#59982,#59983,#59984,#59985,#59986,#59987,#59988));
#63058=AXIS2_PLACEMENT_3D('',#102628,#74214,#74215);
#63059=AXIS2_PLACEMENT_3D('',#102629,#74216,#74217);
#63060=AXIS2_PLACEMENT_3D('',#102645,#74219,#74220);
#63061=AXIS2_PLACEMENT_3D('',#102653,#74221,#74222);
#63062=AXIS2_PLACEMENT_3D('',#102701,#74224,#74225);
#63063=AXIS2_PLACEMENT_3D('',#102749,#74227,#74228);
#63064=AXIS2_PLACEMENT_3D('',#102803,#74230,#74231);
#63065=AXIS2_PLACEMENT_3D('',#102851,#74233,#74234);
#63066=AXIS2_PLACEMENT_3D('',#102905,#74236,#74237);
#63067=AXIS2_PLACEMENT_3D('',#102953,#74239,#74240);
#63068=AXIS2_PLACEMENT_3D('',#103001,#74242,#74243);
#63069=AXIS2_PLACEMENT_3D('',#103055,#74245,#74246);
#63070=AXIS2_PLACEMENT_3D('',#103103,#74248,#74249);
#63071=AXIS2_PLACEMENT_3D('',#103151,#74251,#74252);
#63072=AXIS2_PLACEMENT_3D('',#103166,#74254,#74255);
#63073=AXIS2_PLACEMENT_3D('',#103175,#74256,#74257);
#63074=AXIS2_PLACEMENT_3D('',#103199,#74259,#74260);
#63075=AXIS2_PLACEMENT_3D('',#103224,#74262,#74263);
#63076=AXIS2_PLACEMENT_3D('',#103249,#74265,#74266);
#63077=AXIS2_PLACEMENT_3D('',#103273,#74268,#74269);
#63078=AXIS2_PLACEMENT_3D('',#103298,#74271,#74272);
#63079=AXIS2_PLACEMENT_3D('',#103323,#74274,#74275);
#63080=AXIS2_PLACEMENT_3D('',#103348,#74277,#74278);
#63081=AXIS2_PLACEMENT_3D('',#103373,#74280,#74281);
#63082=AXIS2_PLACEMENT_3D('',#103397,#74283,#74284);
#63083=AXIS2_PLACEMENT_3D('',#103485,#74285,#74286);
#63084=AXIS2_PLACEMENT_3D('',#103487,#74287,#74288);
#63085=AXIS2_PLACEMENT_3D('',#103966,#74289,#74290);
#63086=AXIS2_PLACEMENT_3D('',#103968,#74291,#74292);
#63087=AXIS2_PLACEMENT_3D('',#104055,#74293,#74294);
#63088=AXIS2_PLACEMENT_3D('',#104056,#74295,#74296);
#63089=AXIS2_PLACEMENT_3D('',#104057,#74297,#74298);
#63090=AXIS2_PLACEMENT_3D('',#104361,#74299,#74300);
#63091=AXIS2_PLACEMENT_3D('',#104363,#74301,#74302);
#63092=AXIS2_PLACEMENT_3D('',#104364,#74303,#74304);
#63093=AXIS2_PLACEMENT_3D('',#104365,#74305,#74306);
#63094=AXIS2_PLACEMENT_3D('',#104367,#74307,#74308);
#63095=AXIS2_PLACEMENT_3D('',#104368,#74309,#74310);
#63096=AXIS2_PLACEMENT_3D('',#104369,#74311,#74312);
#63097=AXIS2_PLACEMENT_3D('',#104370,#74313,#74314);
#63098=AXIS2_PLACEMENT_3D('',#104387,#74319,#74320);
#63099=AXIS2_PLACEMENT_3D('',#104404,#74325,#74326);
#63100=AXIS2_PLACEMENT_3D('',#104405,#74327,#74328);
#63101=AXIS2_PLACEMENT_3D('',#104407,#74329,#74330);
#63102=AXIS2_PLACEMENT_3D('',#104408,#74331,#74332);
#63103=AXIS2_PLACEMENT_3D('',#104409,#74333,#74334);
#63104=AXIS2_PLACEMENT_3D('',#104410,#74335,#74336);
#63105=AXIS2_PLACEMENT_3D('',#104411,#74337,#74338);
#63106=AXIS2_PLACEMENT_3D('',#104412,#74339,#74340);
#63107=AXIS2_PLACEMENT_3D('',#104413,#74341,#74342);
#63108=AXIS2_PLACEMENT_3D('',#104414,#74343,#74344);
#63109=AXIS2_PLACEMENT_3D('',#104415,#74345,#74346);
#63110=AXIS2_PLACEMENT_3D('',#104416,#74347,#74348);
#63111=AXIS2_PLACEMENT_3D('',#104417,#74349,#74350);
#63112=AXIS2_PLACEMENT_3D('',#104419,#74352,#74353);
#63113=AXIS2_PLACEMENT_3D('',#104421,#74354,#74355);
#63114=AXIS2_PLACEMENT_3D('',#104423,#74357,#74358);
#74214=DIRECTION('axis',(0.,0.,1.));
#74215=DIRECTION('refdir',(1.,0.,0.));
#74216=DIRECTION('center_axis',(0.,0.,1.));
#74217=DIRECTION('ref_axis',(1.,0.,0.));
#74218=DIRECTION('',(0.,0.,-1.));
#74219=DIRECTION('center_axis',(0.,0.,-1.));
#74220=DIRECTION('ref_axis',(1.,0.,0.));
#74221=DIRECTION('center_axis',(0.,0.,1.));
#74222=DIRECTION('ref_axis',(1.,0.,0.));
#74223=DIRECTION('',(0.,0.,-1.));
#74224=DIRECTION('center_axis',(0.,0.,1.));
#74225=DIRECTION('ref_axis',(1.,0.,0.));
#74226=DIRECTION('',(0.,0.,-1.));
#74227=DIRECTION('center_axis',(0.,0.,1.));
#74228=DIRECTION('ref_axis',(1.,0.,0.));
#74229=DIRECTION('',(0.,0.,-1.));
#74230=DIRECTION('center_axis',(0.,0.,1.));
#74231=DIRECTION('ref_axis',(1.,0.,0.));
#74232=DIRECTION('',(0.,0.,-1.));
#74233=DIRECTION('center_axis',(0.,0.,1.));
#74234=DIRECTION('ref_axis',(1.,0.,0.));
#74235=DIRECTION('',(0.,0.,-1.));
#74236=DIRECTION('center_axis',(0.,0.,1.));
#74237=DIRECTION('ref_axis',(1.,0.,0.));
#74238=DIRECTION('',(0.,0.,-1.));
#74239=DIRECTION('center_axis',(0.,0.,1.));
#74240=DIRECTION('ref_axis',(1.,0.,0.));
#74241=DIRECTION('',(0.,0.,-1.));
#74242=DIRECTION('center_axis',(0.,0.,1.));
#74243=DIRECTION('ref_axis',(1.,0.,0.));
#74244=DIRECTION('',(0.,0.,-1.));
#74245=DIRECTION('center_axis',(0.,0.,1.));
#74246=DIRECTION('ref_axis',(1.,0.,0.));
#74247=DIRECTION('',(0.,0.,-1.));
#74248=DIRECTION('center_axis',(0.,0.,1.));
#74249=DIRECTION('ref_axis',(1.,0.,0.));
#74250=DIRECTION('',(0.,0.,-1.));
#74251=DIRECTION('center_axis',(0.,0.,1.));
#74252=DIRECTION('ref_axis',(1.,5.42442622124796E-14,0.));
#74253=DIRECTION('',(0.,0.,1.));
#74254=DIRECTION('center_axis',(0.,0.,1.));
#74255=DIRECTION('ref_axis',(1.,5.42442622124796E-14,0.));
#74256=DIRECTION('center_axis',(0.,0.,1.));
#74257=DIRECTION('ref_axis',(1.,5.42442622124796E-14,0.));
#74258=DIRECTION('',(0.,0.,1.));
#74259=DIRECTION('center_axis',(0.,0.,1.));
#74260=DIRECTION('ref_axis',(1.,5.42442622124796E-14,0.));
#74261=DIRECTION('',(0.,0.,1.));
#74262=DIRECTION('center_axis',(0.,0.,1.));
#74263=DIRECTION('ref_axis',(1.,5.42442622124796E-14,0.));
#74264=DIRECTION('',(0.,0.,1.));
#74265=DIRECTION('center_axis',(0.,0.,1.));
#74266=DIRECTION('ref_axis',(1.,5.42442622124796E-14,0.));
#74267=DIRECTION('',(0.,0.,1.));
#74268=DIRECTION('center_axis',(0.,0.,1.));
#74269=DIRECTION('ref_axis',(1.,5.42442622124796E-14,0.));
#74270=DIRECTION('',(0.,0.,1.));
#74271=DIRECTION('center_axis',(0.,0.,1.));
#74272=DIRECTION('ref_axis',(1.,5.42442622124796E-14,0.));
#74273=DIRECTION('',(0.,0.,1.));
#74274=DIRECTION('center_axis',(0.,0.,1.));
#74275=DIRECTION('ref_axis',(1.,5.42442622124796E-14,0.));
#74276=DIRECTION('',(0.,0.,1.));
#74277=DIRECTION('center_axis',(0.,0.,1.));
#74278=DIRECTION('ref_axis',(1.,5.42442622124796E-14,0.));
#74279=DIRECTION('',(0.,0.,1.));
#74280=DIRECTION('center_axis',(0.,0.,1.));
#74281=DIRECTION('ref_axis',(1.,5.42442622124796E-14,0.));
#74282=DIRECTION('',(0.,0.,1.));
#74283=DIRECTION('center_axis',(0.,0.,1.));
#74284=DIRECTION('ref_axis',(1.,0.,0.));
#74285=DIRECTION('center_axis',(0.,0.,-1.));
#74286=DIRECTION('ref_axis',(1.,0.,0.));
#74287=DIRECTION('center_axis',(0.,0.,-1.));
#74288=DIRECTION('ref_axis',(1.,0.,0.));
#74289=DIRECTION('center_axis',(0.,0.,1.));
#74290=DIRECTION('ref_axis',(1.,0.,0.));
#74291=DIRECTION('center_axis',(0.,0.,-1.));
#74292=DIRECTION('ref_axis',(1.,0.,0.));
#74293=DIRECTION('center_axis',(0.,0.,-1.));
#74294=DIRECTION('ref_axis',(1.,5.42442622124796E-14,0.));
#74295=DIRECTION('center_axis',(0.,0.,-1.));
#74296=DIRECTION('ref_axis',(1.,0.,0.));
#74297=DIRECTION('center_axis',(0.,0.,1.));
#74298=DIRECTION('ref_axis',(0.889182919820768,0.457551893339995,0.));
#74299=DIRECTION('center_axis',(0.,0.,1.));
#74300=DIRECTION('ref_axis',(1.,0.,0.));
#74301=DIRECTION('center_axis',(0.,0.,1.));
#74302=DIRECTION('ref_axis',(1.,0.,0.));
#74303=DIRECTION('center_axis',(0.,-1.,0.));
#74304=DIRECTION('ref_axis',(-1.,0.,0.));
#74305=DIRECTION('center_axis',(0.,0.,1.));
#74306=DIRECTION('ref_axis',(1.,0.,0.));
#74307=DIRECTION('center_axis',(0.,0.,1.));
#74308=DIRECTION('ref_axis',(1.,0.,0.));
#74309=DIRECTION('center_axis',(0.,0.,1.));
#74310=DIRECTION('ref_axis',(1.,0.,0.));
#74311=DIRECTION('center_axis',(0.,0.,-1.));
#74312=DIRECTION('ref_axis',(1.,0.,0.));
#74313=DIRECTION('center_axis',(0.,1.,0.));
#74314=DIRECTION('ref_axis',(-1.,0.,0.));
#74315=DIRECTION('',(0.,0.,-1.));
#74316=DIRECTION('',(-1.,0.,0.));
#74317=DIRECTION('',(0.,0.,1.));
#74318=DIRECTION('',(-1.,0.,0.));
#74319=DIRECTION('center_axis',(0.,-1.,0.));
#74320=DIRECTION('ref_axis',(1.,0.,0.));
#74321=DIRECTION('',(0.,0.,1.));
#74322=DIRECTION('',(1.,0.,0.));
#74323=DIRECTION('',(0.,0.,-1.));
#74324=DIRECTION('',(1.,0.,0.));
#74325=DIRECTION('center_axis',(0.,0.,1.));
#74326=DIRECTION('ref_axis',(1.,0.,0.));
#74327=DIRECTION('center_axis',(0.,0.,1.));
#74328=DIRECTION('ref_axis',(1.,0.,0.));
#74329=DIRECTION('center_axis',(0.,0.,1.));
#74330=DIRECTION('ref_axis',(1.,0.,0.));
#74331=DIRECTION('center_axis',(0.,0.,1.));
#74332=DIRECTION('ref_axis',(1.,0.,0.));
#74333=DIRECTION('center_axis',(0.,0.,1.));
#74334=DIRECTION('ref_axis',(1.,0.,0.));
#74335=DIRECTION('center_axis',(0.,0.,1.));
#74336=DIRECTION('ref_axis',(1.,0.,0.));
#74337=DIRECTION('center_axis',(0.,0.,1.));
#74338=DIRECTION('ref_axis',(1.,0.,0.));
#74339=DIRECTION('center_axis',(0.,0.,1.));
#74340=DIRECTION('ref_axis',(1.,0.,0.));
#74341=DIRECTION('center_axis',(0.,0.,1.));
#74342=DIRECTION('ref_axis',(1.,0.,0.));
#74343=DIRECTION('center_axis',(0.,0.,1.));
#74344=DIRECTION('ref_axis',(1.,0.,0.));
#74345=DIRECTION('center_axis',(0.,0.,-1.));
#74346=DIRECTION('ref_axis',(-1.,0.,0.));
#74347=DIRECTION('center_axis',(0.,0.,-1.));
#74348=DIRECTION('ref_axis',(-1.,0.,0.));
#74349=DIRECTION('center_axis',(0.,0.,1.));
#74350=DIRECTION('ref_axis',(1.,0.,0.));
#74351=DIRECTION('',(0.,0.,-1.));
#74352=DIRECTION('center_axis',(0.,0.,-1.));
#74353=DIRECTION('ref_axis',(1.,0.,0.));
#74354=DIRECTION('center_axis',(0.,0.,1.));
#74355=DIRECTION('ref_axis',(1.,0.,0.));
#74356=DIRECTION('',(-0.70710678118654,-8.65956056235484E-17,-0.707106781186555));
#74357=DIRECTION('center_axis',(0.,0.,1.));
#74358=DIRECTION('ref_axis',(1.,0.,0.));
#102628=CARTESIAN_POINT('',(0.,0.,0.));
#102629=CARTESIAN_POINT('Origin',(110.,10.75,10.13));
#102630=CARTESIAN_POINT('',(108.044515157092,10.751507398398,6.80586969212423));
#102631=CARTESIAN_POINT('',(108.044569492149,10.7516873045422,6.70413030787577));
#102632=CARTESIAN_POINT('',(108.046,10.75,10.13));
#102633=CARTESIAN_POINT('',(110.862570875312,12.5048480452433,6.58));
#102634=CARTESIAN_POINT('Ctrl Pts',(108.044515157092,10.751507398398,6.80586969212423));
#102635=CARTESIAN_POINT('Ctrl Pts',(108.043711910884,10.8492225887016,6.80028600079932));
#102636=CARTESIAN_POINT('Ctrl Pts',(108.05041787597,10.9468235741413,6.79470230947441));
#102637=CARTESIAN_POINT('Ctrl Pts',(108.065019752885,11.0432231509002,6.7891186181495));
#102638=CARTESIAN_POINT('Ctrl Pts',(108.160730597505,11.675092941758,6.75251922644771));
#102639=CARTESIAN_POINT('Ctrl Pts',(108.595681572202,12.2553453835437,6.71591983474591));
#102640=CARTESIAN_POINT('Ctrl Pts',(109.175396647758,12.5247754482411,6.67932044304411));
#102641=CARTESIAN_POINT('Ctrl Pts',(109.699791138726,12.7684945571377,6.64621362869607));
#102642=CARTESIAN_POINT('Ctrl Pts',(110.342639138428,12.7578826479092,6.61310681434804));
#102643=CARTESIAN_POINT('Ctrl Pts',(110.863615890953,12.505874778859,6.58));
#102644=CARTESIAN_POINT('',(109.138474140329,12.5038213116275,6.58));
#102645=CARTESIAN_POINT('Origin',(110.,10.75,6.58));
#102646=CARTESIAN_POINT('Ctrl Pts',(109.13847414033,12.5038213116275,6.58));
#102647=CARTESIAN_POINT('Ctrl Pts',(108.562316880239,12.2207968236057,6.6165993917018));
#102648=CARTESIAN_POINT('Ctrl Pts',(108.141185267799,11.6340572295968,6.65319878340359));
#102649=CARTESIAN_POINT('Ctrl Pts',(108.059472317674,11.0011909565928,6.68979817510539));
#102650=CARTESIAN_POINT('Ctrl Pts',(108.048806194589,10.918581901917,6.69457555269552));
#102651=CARTESIAN_POINT('Ctrl Pts',(108.043923256952,10.8351869177435,6.69935293028564));
#102652=CARTESIAN_POINT('Ctrl Pts',(108.044569492149,10.7516873045422,6.70413030787577));
#102653=CARTESIAN_POINT('Origin',(110.,10.75,10.13));
#102654=CARTESIAN_POINT('',(108.048945433675,10.7497217851578,7.50586969212423));
#102655=CARTESIAN_POINT('',(108.048986005899,10.7499472362473,7.40413030787577));
#102656=CARTESIAN_POINT('',(108.046,10.75,10.13));
#102657=CARTESIAN_POINT('Ctrl Pts',(108.048945433675,10.7497217851578,7.50586969212423));
#102658=CARTESIAN_POINT('Ctrl Pts',(108.049389547632,11.0898217190185,7.48654901767677));
#102659=CARTESIAN_POINT('Ctrl Pts',(108.134132298949,11.4301285218672,7.46722834322932));
#102660=CARTESIAN_POINT('Ctrl Pts',(108.301860293071,11.7228908251559,7.44790766878186));
#102661=CARTESIAN_POINT('Ctrl Pts',(108.619589499312,12.2774740640964,7.41130827708006));
#102662=CARTESIAN_POINT('Ctrl Pts',(109.235104542373,12.6614477089837,7.37470888537826));
#102663=CARTESIAN_POINT('Ctrl Pts',(109.872908683461,12.7029554058002,7.33810949367646));
#102664=CARTESIAN_POINT('Ctrl Pts',(110.51071282455,12.7444631026166,7.30151010197467));
#102665=CARTESIAN_POINT('Ctrl Pts',(111.170806063666,12.4435048513622,7.26491071027287));
#102666=CARTESIAN_POINT('Ctrl Pts',(111.557730049867,11.9347725404045,7.22831131857107));
#102667=CARTESIAN_POINT('Ctrl Pts',(111.944654036068,11.4260402294468,7.19171192686928));
#102668=CARTESIAN_POINT('Ctrl Pts',(112.058408769352,10.7095338587858,7.15511253516748));
#102669=CARTESIAN_POINT('Ctrl Pts',(111.848090495719,10.1059857264717,7.11851314346568));
#102670=CARTESIAN_POINT('Ctrl Pts',(111.637772222086,9.50243759415752,7.08191375176388));
#102671=CARTESIAN_POINT('Ctrl Pts',(111.103380941534,9.01184770019013,7.04531436006208));
#102672=CARTESIAN_POINT('Ctrl Pts',(110.484081604292,8.85373963219972,7.00871496836028));
#102673=CARTESIAN_POINT('Ctrl Pts',(109.864782267049,8.69563156420931,6.97211557665849));
#102674=CARTESIAN_POINT('Ctrl Pts',(109.160574873114,8.87000532219587,6.93551618495669));
#102675=CARTESIAN_POINT('Ctrl Pts',(108.686706533419,9.29893577115414,6.89891679325489));
#102676=CARTESIAN_POINT('Ctrl Pts',(108.285132688644,9.66242755800698,6.86790109287801));
#102677=CARTESIAN_POINT('Ctrl Pts',(108.048976944515,10.2087293527696,6.83688539250112));
#102678=CARTESIAN_POINT('Ctrl Pts',(108.044515157092,10.751507398398,6.80586969212423));
#102679=CARTESIAN_POINT('Ctrl Pts',(108.044569492149,10.7516873045422,6.70413030787577));
#102680=CARTESIAN_POINT('Ctrl Pts',(108.048874051536,10.1954980941472,6.73595232198744));
#102681=CARTESIAN_POINT('Ctrl Pts',(108.29850053233,9.63466663527941,6.76777433609911));
#102682=CARTESIAN_POINT('Ctrl Pts',(108.718378388755,9.27054355030639,6.79959635021079));
#102683=CARTESIAN_POINT('Ctrl Pts',(109.201291697771,8.85175536902323,6.83619574191258));
#102684=CARTESIAN_POINT('Ctrl Pts',(109.909412603614,8.69317195845609,6.87279513361438));
#102685=CARTESIAN_POINT('Ctrl Pts',(110.525208044422,8.86480594334321,6.90939452531618));
#102686=CARTESIAN_POINT('Ctrl Pts',(111.14100348523,9.03643992823033,6.94599391701798));
#102687=CARTESIAN_POINT('Ctrl Pts',(111.664473461004,9.53829130857172,6.98259330871977));
#102688=CARTESIAN_POINT('Ctrl Pts',(111.861602039404,10.1462061785723,7.01919270042156));
#102689=CARTESIAN_POINT('Ctrl Pts',(112.058730617804,10.7541210485729,7.05579209212336));
#102690=CARTESIAN_POINT('Ctrl Pts',(111.929517798829,11.4680994082327,7.09239148382517));
#102691=CARTESIAN_POINT('Ctrl Pts',(111.531658092341,11.9683395872945,7.12899087552696));
#102692=CARTESIAN_POINT('Ctrl Pts',(111.133798385853,12.4685797663562,7.16559026722876));
#102693=CARTESIAN_POINT('Ctrl Pts',(110.46729179185,12.7550817648198,7.20218965893055));
#102694=CARTESIAN_POINT('Ctrl Pts',(109.830530205499,12.6997228916506,7.23878905063235));
#102695=CARTESIAN_POINT('Ctrl Pts',(109.193768619148,12.6443640184814,7.27538844233415));
#102696=CARTESIAN_POINT('Ctrl Pts',(108.586752040449,12.2471442736793,7.31198783403595));
#102697=CARTESIAN_POINT('Ctrl Pts',(108.281142413997,11.6858003617248,7.34858722573775));
#102698=CARTESIAN_POINT('Ctrl Pts',(108.126545121574,11.4018359790796,7.36710158645042));
#102699=CARTESIAN_POINT('Ctrl Pts',(108.049077765418,11.0758722780451,7.38561594716309));
#102700=CARTESIAN_POINT('Ctrl Pts',(108.048986005899,10.7499472362473,7.40413030787577));
#102701=CARTESIAN_POINT('Origin',(110.,10.75,10.13));
#102702=CARTESIAN_POINT('',(108.043619792706,10.7489886882952,8.20586969212423));
#102703=CARTESIAN_POINT('',(108.043932396619,10.7488069461449,8.10413030787577));
#102704=CARTESIAN_POINT('',(108.046,10.75,10.13));
#102705=CARTESIAN_POINT('Ctrl Pts',(108.043619792706,10.7489886882952,8.20586969212423));
#102706=CARTESIAN_POINT('Ctrl Pts',(108.047304171251,11.3268472727125,8.17281203455422));
#102707=CARTESIAN_POINT('Ctrl Pts',(108.319782513348,11.9077308098779,8.13975437698421));
#102708=CARTESIAN_POINT('Ctrl Pts',(108.768450547222,12.2710129638945,8.10669671941421));
#102709=CARTESIAN_POINT('Ctrl Pts',(109.265188015117,12.6732164722637,8.07009732771241));
#102710=CARTESIAN_POINT('Ctrl Pts',(109.977890832777,12.8086940538942,8.03349793601062));
#102711=CARTESIAN_POINT('Ctrl Pts',(110.587558939682,12.616807124334,7.99689854430882));
#102712=CARTESIAN_POINT('Ctrl Pts',(111.197227046588,12.4249201947739,7.96029915260702));
#102713=CARTESIAN_POINT('Ctrl Pts',(111.703860442739,11.9056687540232,7.92369976090523));
#102714=CARTESIAN_POINT('Ctrl Pts',(111.880693974763,11.2914654024873,7.88710036920343));
#102715=CARTESIAN_POINT('Ctrl Pts',(112.057527506788,10.6772620509515,7.85050097750163));
#102716=CARTESIAN_POINT('Ctrl Pts',(111.904561174686,9.96810678863055,7.81390158579984));
#102717=CARTESIAN_POINT('Ctrl Pts',(111.490261658278,9.48141227895056,7.77730219409804));
#102718=CARTESIAN_POINT('Ctrl Pts',(111.075962141869,8.99471776927057,7.74070280239624));
#102719=CARTESIAN_POINT('Ctrl Pts',(110.400329441155,8.73048401223154,7.70410341069444));
#102720=CARTESIAN_POINT('Ctrl Pts',(109.765771025388,8.80697907788465,7.66750401899264));
#102721=CARTESIAN_POINT('Ctrl Pts',(109.131212609621,8.88347414353777,7.63090462729084));
#102722=CARTESIAN_POINT('Ctrl Pts',(108.537728478803,9.30069803188303,7.59430523558905));
#102723=CARTESIAN_POINT('Ctrl Pts',(108.250958098105,9.87190639255244,7.55770584388725));
#102724=CARTESIAN_POINT('Ctrl Pts',(108.115572669697,10.14157611378,7.54042712663291));
#102725=CARTESIAN_POINT('Ctrl Pts',(108.04854825709,10.4455662231262,7.52314840937857));
#102726=CARTESIAN_POINT('Ctrl Pts',(108.048945433675,10.7497217851578,7.50586969212423));
#102727=CARTESIAN_POINT('Ctrl Pts',(108.048986005899,10.7499472362473,7.40413030787577));
#102728=CARTESIAN_POINT('Ctrl Pts',(108.048896374192,10.4315800739931,7.42221533886489));
#102729=CARTESIAN_POINT('Ctrl Pts',(108.12263541912,10.113249798825,7.44030036985402));
#102730=CARTESIAN_POINT('Ctrl Pts',(108.270432104423,9.83413722201615,7.45838540084314));
#102731=CARTESIAN_POINT('Ctrl Pts',(108.569534095507,9.26928607336913,7.49498479254494));
#102732=CARTESIAN_POINT('Ctrl Pts',(109.171940751879,8.86505185518214,7.53158418424673));
#102733=CARTESIAN_POINT('Ctrl Pts',(109.808011482606,8.80235313266459,7.56818357594853));
#102734=CARTESIAN_POINT('Ctrl Pts',(110.444082213333,8.73965441014704,7.60478296765033));
#102735=CARTESIAN_POINT('Ctrl Pts',(111.113817018416,9.01849118329893,7.64138235935213));
#102736=CARTESIAN_POINT('Ctrl Pts',(111.51745195286,9.51406494419263,7.67798175105392));
#102737=CARTESIAN_POINT('Ctrl Pts',(111.921086887305,10.0096387050863,7.71458114275572));
#102738=CARTESIAN_POINT('Ctrl Pts',(112.058621951111,10.7219494537218,7.75118053445752));
#102739=CARTESIAN_POINT('Ctrl Pts',(111.868495572048,11.3321693276087,7.78777992615932));
#102740=CARTESIAN_POINT('Ctrl Pts',(111.678369192984,11.9423892014956,7.82437931786111));
#102741=CARTESIAN_POINT('Ctrl Pts',(111.160581371051,12.4505182006339,7.86097870956291));
#102742=CARTESIAN_POINT('Ctrl Pts',(110.5468907788,12.6291234308646,7.89757810126471));
#102743=CARTESIAN_POINT('Ctrl Pts',(109.933200186548,12.8077286610953,7.93417749296651));
#102744=CARTESIAN_POINT('Ctrl Pts',(109.223606823978,12.6568101224185,7.9707768846683));
#102745=CARTESIAN_POINT('Ctrl Pts',(108.735718548346,12.2439169655075,8.0073762763701));
#102746=CARTESIAN_POINT('Ctrl Pts',(108.305791934843,11.880075968388,8.03962762020532));
#102747=CARTESIAN_POINT('Ctrl Pts',(108.048021872612,11.3128086655436,8.07187896404054));
#102748=CARTESIAN_POINT('Ctrl Pts',(108.043932396619,10.7488069461449,8.10413030787577));
#102749=CARTESIAN_POINT('Origin',(110.,10.75,10.13));
#102750=CARTESIAN_POINT('',(108.046780828974,10.7516319787095,8.90586969212423));
#102751=CARTESIAN_POINT('',(108.046385982006,10.751669101789,8.80413030787576));
#102752=CARTESIAN_POINT('',(108.046,10.75,10.13));
#102753=CARTESIAN_POINT('Ctrl Pts',(108.046780828974,10.7516319787095,8.90586969212423));
#102754=CARTESIAN_POINT('Ctrl Pts',(108.045300812305,10.930595849109,8.89567444313347));
#102755=CARTESIAN_POINT('Ctrl Pts',(108.067935018338,11.1091924125775,8.88547919414272));
#102756=CARTESIAN_POINT('Ctrl Pts',(108.116203099833,11.2805692246058,8.87528394515196));
#102757=CARTESIAN_POINT('Ctrl Pts',(108.289478163829,11.8957858885357,8.83868455345016));
#102758=CARTESIAN_POINT('Ctrl Pts',(108.793097157889,12.4179615658071,8.80208516174836));
#102759=CARTESIAN_POINT('Ctrl Pts',(109.401644233603,12.6133745840746,8.76548577004656));
#102760=CARTESIAN_POINT('Ctrl Pts',(110.010191309318,12.808787602342,8.72888637834476));
#102761=CARTESIAN_POINT('Ctrl Pts',(110.723666466687,12.6774379616055,8.69228698664297));
#102762=CARTESIAN_POINT('Ctrl Pts',(111.222723911923,12.2781167156913,8.65568759494117));
#102763=CARTESIAN_POINT('Ctrl Pts',(111.721781357158,11.8787954697771,8.61908820323938));
#102764=CARTESIAN_POINT('Ctrl Pts',(112.006421090259,11.2115026186853,8.58248881153758));
#102765=CARTESIAN_POINT('Ctrl Pts',(111.94924063397,10.5749131216331,8.54588941983578));
#102766=CARTESIAN_POINT('Ctrl Pts',(111.892060177682,9.93832362458086,8.50929002813398));
#102767=CARTESIAN_POINT('Ctrl Pts',(111.493059532004,9.33243748156825,8.47269063643218));
#102768=CARTESIAN_POINT('Ctrl Pts',(110.930828208466,9.02844450748747,8.43609124473038));
#102769=CARTESIAN_POINT('Ctrl Pts',(110.368596884928,8.72445153340668,8.39949185302859));
#102770=CARTESIAN_POINT('Ctrl Pts',(109.643134883529,8.72235172825773,8.36289246132679));
#102771=CARTESIAN_POINT('Ctrl Pts',(109.079153209653,9.02308493605,8.326293069625));
#102772=CARTESIAN_POINT('Ctrl Pts',(108.515171535777,9.32381814384228,8.2896936779232));
#102773=CARTESIAN_POINT('Ctrl Pts',(108.112670189424,9.9273843645758,8.2530942862214));
#102774=CARTESIAN_POINT('Ctrl Pts',(108.051805575312,10.5636321924966,8.2164948945196));
#102775=CARTESIAN_POINT('Ctrl Pts',(108.045915688317,10.6252020859741,8.21295316038781));
#102776=CARTESIAN_POINT('Ctrl Pts',(108.043225055443,10.6870780260698,8.20941142625602));
#102777=CARTESIAN_POINT('Ctrl Pts',(108.043619792706,10.7489886882952,8.20586969212423));
#102778=CARTESIAN_POINT('Ctrl Pts',(108.043932396619,10.7488069461449,8.10413030787577));
#102779=CARTESIAN_POINT('Ctrl Pts',(108.043381063396,10.6727696037847,8.10847835574234));
#102780=CARTESIAN_POINT('Ctrl Pts',(108.047440572113,10.5967916159432,8.11282640360892));
#102781=CARTESIAN_POINT('Ctrl Pts',(108.056310690425,10.5213794633641,8.11717445147549));
#102782=CARTESIAN_POINT('Ctrl Pts',(108.130974296833,9.88660289327707,8.15377384317729));
#102783=CARTESIAN_POINT('Ctrl Pts',(108.546484698346,9.29191752824843,8.19037323487909));
#102784=CARTESIAN_POINT('Ctrl Pts',(109.116862635547,9.00349960882683,8.22697262658088));
#102785=CARTESIAN_POINT('Ctrl Pts',(109.687240572748,8.71508168940523,8.26357201828268));
#102786=CARTESIAN_POINT('Ctrl Pts',(110.412486045638,8.73293121559066,8.30017140998448));
#102787=CARTESIAN_POINT('Ctrl Pts',(110.967985017009,9.04905897482588,8.33677080168628));
#102788=CARTESIAN_POINT('Ctrl Pts',(111.52348398838,9.36518673406111,8.37337019338807));
#102789=CARTESIAN_POINT('Ctrl Pts',(111.909236458231,9.97959272634614,8.40996958508987));
#102790=CARTESIAN_POINT('Ctrl Pts',(111.952582667526,10.6172736803138,8.44656897679167));
#102791=CARTESIAN_POINT('Ctrl Pts',(111.99592887682,11.2549546342814,8.48316836849346));
#102792=CARTESIAN_POINT('Ctrl Pts',(111.696868825557,11.9159105499316,8.51976776019526));
#102793=CARTESIAN_POINT('Ctrl Pts',(111.189259422973,12.3043028494267,8.55636715189706));
#102794=CARTESIAN_POINT('Ctrl Pts',(110.68165002039,12.6926951489219,8.59296654359886));
#102795=CARTESIAN_POINT('Ctrl Pts',(109.965491266485,12.808523832262,8.62956593530066));
#102796=CARTESIAN_POINT('Ctrl Pts',(109.361330105331,12.599944892835,8.66616532700245));
#102797=CARTESIAN_POINT('Ctrl Pts',(108.757168944176,12.391365953408,8.70276471870425));
#102798=CARTESIAN_POINT('Ctrl Pts',(108.265005375772,11.8583793912139,8.73936411040605));
#102799=CARTESIAN_POINT('Ctrl Pts',(108.105127894314,11.2395457492598,8.77596350210785));
#102800=CARTESIAN_POINT('Ctrl Pts',(108.064114116421,11.0807947774987,8.78535243736382));
#102801=CARTESIAN_POINT('Ctrl Pts',(108.044967736627,10.9163942996569,8.79474137261979));
#102802=CARTESIAN_POINT('Ctrl Pts',(108.046385982006,10.751669101789,8.80413030787576));
#102803=CARTESIAN_POINT('Origin',(110.,10.75,10.13));
#102804=CARTESIAN_POINT('',(108.04785445166,10.7486597361157,9.60586969212423));
#102805=CARTESIAN_POINT('',(108.048142496813,10.7488058307817,9.50413030787576));
#102806=CARTESIAN_POINT('',(108.046,10.75,10.13));
#102807=CARTESIAN_POINT('Ctrl Pts',(108.04785445166,10.7486597361157,9.60586969212423));
#102808=CARTESIAN_POINT('Ctrl Pts',(108.050592274151,11.169344087362,9.58193746001092));
#102809=CARTESIAN_POINT('Ctrl Pts',(108.184359614202,11.5916163945113,9.55800522789762));
#102810=CARTESIAN_POINT('Ctrl Pts',(108.435439206868,11.9257312565921,9.53407299578431));
#102811=CARTESIAN_POINT('Ctrl Pts',(108.819413435298,12.4366907296905,9.49747360408251));
#102812=CARTESIAN_POINT('Ctrl Pts',(109.47775012871,12.741473154812,9.46087421238071));
#102813=CARTESIAN_POINT('Ctrl Pts',(110.115783029776,12.7036603474404,9.42427482067892));
#102814=CARTESIAN_POINT('Ctrl Pts',(110.753815930842,12.6658475400688,9.38767542897712));
#102815=CARTESIAN_POINT('Ctrl Pts',(111.371545039561,12.2854395002041,9.35107603727532));
#102816=CARTESIAN_POINT('Ctrl Pts',(111.692479729901,11.7327038348298,9.31447664557353));
#102817=CARTESIAN_POINT('Ctrl Pts',(112.013414420241,11.1799681694555,9.27787725387173));
#102818=CARTESIAN_POINT('Ctrl Pts',(112.037554692202,10.4549048785716,9.24127786216993));
#102819=CARTESIAN_POINT('Ctrl Pts',(111.754095552424,9.88204651271007,9.20467847046813));
#102820=CARTESIAN_POINT('Ctrl Pts',(111.470636412645,9.30918814684853,9.16807907876633));
#102821=CARTESIAN_POINT('Ctrl Pts',(110.879577861129,8.88853470600938,9.13147968706454));
#102822=CARTESIAN_POINT('Ctrl Pts',(110.245472995097,8.80836731797791,9.09488029536274));
#102823=CARTESIAN_POINT('Ctrl Pts',(109.611368129065,8.72819992994645,9.05828090366094));
#102824=CARTESIAN_POINT('Ctrl Pts',(108.934216948517,8.98851859472268,9.02168151195914));
#102825=CARTESIAN_POINT('Ctrl Pts',(108.51710692521,9.47280675240502,8.98508212025735));
#102826=CARTESIAN_POINT('Ctrl Pts',(108.216188465381,9.82218998076296,8.95867797754631));
#102827=CARTESIAN_POINT('Ctrl Pts',(108.050613846824,10.2881428007179,8.93227383483527));
#102828=CARTESIAN_POINT('Ctrl Pts',(108.046780828974,10.7516319787095,8.90586969212423));
#102829=CARTESIAN_POINT('Ctrl Pts',(108.046385982006,10.751669101789,8.80413030787576));
#102830=CARTESIAN_POINT('Ctrl Pts',(108.050496256821,10.2742722830963,8.83134076432159));
#102831=CARTESIAN_POINT('Ctrl Pts',(108.227333346095,9.79414806941248,8.85855122076741));
#102832=CARTESIAN_POINT('Ctrl Pts',(108.545184991362,9.44091305650114,8.88576167721324));
#102833=CARTESIAN_POINT('Ctrl Pts',(108.972710964378,8.96579472741058,8.92236106891503));
#102834=CARTESIAN_POINT('Ctrl Pts',(109.655354304921,8.72023879094344,8.95896046061684));
#102835=CARTESIAN_POINT('Ctrl Pts',(110.287569294919,8.81415412860432,8.99555985231863));
#102836=CARTESIAN_POINT('Ctrl Pts',(110.919784284918,8.9080694662652,9.03215924402043));
#102837=CARTESIAN_POINT('Ctrl Pts',(111.501570924371,9.34145607805408,9.06875863572223));
#102838=CARTESIAN_POINT('Ctrl Pts',(111.772526149646,9.92033356978501,9.10535802742402));
#102839=CARTESIAN_POINT('Ctrl Pts',(112.043481374921,10.4992110615159,9.14195741912582));
#102840=CARTESIAN_POINT('Ctrl Pts',(112.003605186016,11.2235794331889,9.17855681082762));
#102841=CARTESIAN_POINT('Ctrl Pts',(111.670745847484,11.7692171748484,9.21515620252942));
#102842=CARTESIAN_POINT('Ctrl Pts',(111.337886508951,12.3148549165078,9.25175559423121));
#102843=CARTESIAN_POINT('Ctrl Pts',(110.71204402079,12.6817620281538,9.28835498593301));
#102844=CARTESIAN_POINT('Ctrl Pts',(110.073340492925,12.7057138105415,9.3249543776348));
#102845=CARTESIAN_POINT('Ctrl Pts',(109.434636965061,12.7296655929293,9.3615537693366));
#102846=CARTESIAN_POINT('Ctrl Pts',(108.783072397493,12.410662046059,9.39815316103841));
#102847=CARTESIAN_POINT('Ctrl Pts',(108.410281898036,11.8914866152722,9.4347525527402));
#102848=CARTESIAN_POINT('Ctrl Pts',(108.174728183565,11.5634372112182,9.45787847111873));
#102849=CARTESIAN_POINT('Ctrl Pts',(108.050476378586,11.1554682039619,9.48100438949724));
#102850=CARTESIAN_POINT('Ctrl Pts',(108.048142496813,10.7488058307817,9.50413030787576));
#102851=CARTESIAN_POINT('Origin',(110.,10.75,10.13));
#102852=CARTESIAN_POINT('',(108.042985073083,10.7503289497149,10.3058696921242));
#102853=CARTESIAN_POINT('',(108.042916139437,10.7500816311095,10.2041303078758));
#102854=CARTESIAN_POINT('',(108.046,10.75,10.13));
#102855=CARTESIAN_POINT('Ctrl Pts',(108.042985073083,10.7503289497149,10.3058696921242));
#102856=CARTESIAN_POINT('Ctrl Pts',(108.042940614159,10.769013669924,10.3047998685902));
#102857=CARTESIAN_POINT('Ctrl Pts',(108.043185641729,10.7876971962134,10.3037300450561));
#102858=CARTESIAN_POINT('Ctrl Pts',(108.043723784935,10.8063722760494,10.3026602215221));
#102859=CARTESIAN_POINT('Ctrl Pts',(108.062134030542,11.4452594758757,10.2660608298203));
#102860=CARTESIAN_POINT('Ctrl Pts',(108.423598228993,12.074261194306,10.2294614381185));
#102861=CARTESIAN_POINT('Ctrl Pts',(108.966327885768,12.4118412750302,10.1928620464167));
#102862=CARTESIAN_POINT('Ctrl Pts',(109.509057542544,12.7494213557543,10.1562626547149));
#102863=CARTESIAN_POINT('Ctrl Pts',(110.233052657643,12.7955797987723,10.1196632630131));
#102864=CARTESIAN_POINT('Ctrl Pts',(110.814258787462,12.5296564528512,10.0830638713113));
#102865=CARTESIAN_POINT('Ctrl Pts',(111.395464917281,12.26373310693,10.0464644796095));
#102866=CARTESIAN_POINT('Ctrl Pts',(111.83388206182,11.6857279720698,10.0098650879077));
#102867=CARTESIAN_POINT('Ctrl Pts',(111.933278201169,11.0543515401945,9.97326569620588));
#102868=CARTESIAN_POINT('Ctrl Pts',(112.032674340518,10.4229751083192,9.93666630450408));
#102869=CARTESIAN_POINT('Ctrl Pts',(111.793049474678,9.73822737942879,9.90006691280229));
#102870=CARTESIAN_POINT('Ctrl Pts',(111.321657783896,9.3065959798443,9.86346752110049));
#102871=CARTESIAN_POINT('Ctrl Pts',(110.850266093114,8.87496458025981,9.82686812939869));
#102872=CARTESIAN_POINT('Ctrl Pts',(110.147107577391,8.6964495099812,9.79026873769689));
#102873=CARTESIAN_POINT('Ctrl Pts',(109.526910384509,8.85095269178194,9.75366934599509));
#102874=CARTESIAN_POINT('Ctrl Pts',(108.906713191627,9.00545587358267,9.7170699542933));
#102875=CARTESIAN_POINT('Ctrl Pts',(108.369477321586,9.49297730746276,9.6804705625915));
#102876=CARTESIAN_POINT('Ctrl Pts',(108.155665268289,10.0953062849405,9.6438711708897));
#102877=CARTESIAN_POINT('Ctrl Pts',(108.081664273324,10.3037741563371,9.63120401130121));
#102878=CARTESIAN_POINT('Ctrl Pts',(108.046405341763,10.5259945125633,9.61853685171272));
#102879=CARTESIAN_POINT('Ctrl Pts',(108.04785445166,10.7486597361157,9.60586969212423));
#102880=CARTESIAN_POINT('Ctrl Pts',(108.048142496813,10.7488058307817,9.50413030787576));
#102881=CARTESIAN_POINT('Ctrl Pts',(108.046782745676,10.5118788233028,9.51760378119904));
#102882=CARTESIAN_POINT('Ctrl Pts',(108.086806636952,10.2753953377931,9.53107725452231));
#102883=CARTESIAN_POINT('Ctrl Pts',(108.170313609378,10.0554187963128,9.54455072784559));
#102884=CARTESIAN_POINT('Ctrl Pts',(108.397152251522,9.45787372284372,9.58115011954739));
#102885=CARTESIAN_POINT('Ctrl Pts',(108.944845967157,8.98213089060881,9.61774951124919));
#102886=CARTESIAN_POINT('Ctrl Pts',(109.568251414047,8.84112899987964,9.65434890295099));
#102887=CARTESIAN_POINT('Ctrl Pts',(110.191656860937,8.70012710915047,9.69094829465279));
#102888=CARTESIAN_POINT('Ctrl Pts',(110.890774039081,8.89386615992705,9.72754768635458));
#102889=CARTESIAN_POINT('Ctrl Pts',(111.352683671185,9.33563009708535,9.76414707805638));
#102890=CARTESIAN_POINT('Ctrl Pts',(111.814593303289,9.77739403424364,9.80074646975817));
#102891=CARTESIAN_POINT('Ctrl Pts',(112.039295389352,10.4671828577836,9.83734586145997));
#102892=CARTESIAN_POINT('Ctrl Pts',(111.92621506643,11.0962525875984,9.87394525316177));
#102893=CARTESIAN_POINT('Ctrl Pts',(111.813134743508,11.7253223174132,9.91054464486356));
#102894=CARTESIAN_POINT('Ctrl Pts',(111.3622720116,12.2936729535027,9.94714403656536));
#102895=CARTESIAN_POINT('Ctrl Pts',(110.775429436335,12.5469152806487,9.98374342826716));
#102896=CARTESIAN_POINT('Ctrl Pts',(110.18858686107,12.8001576077948,10.020342819969));
#102897=CARTESIAN_POINT('Ctrl Pts',(109.465764442448,12.7382916259973,10.0569422116708));
#102898=CARTESIAN_POINT('Ctrl Pts',(108.930491734476,12.3890080556661,10.0935416033726));
#102899=CARTESIAN_POINT('Ctrl Pts',(108.395219026505,12.0397244853349,10.1301409950744));
#102900=CARTESIAN_POINT('Ctrl Pts',(108.047496029185,11.4030233264699,10.1667403867761));
#102901=CARTESIAN_POINT('Ctrl Pts',(108.04296078492,10.7638869435582,10.2033397784779));
#102902=CARTESIAN_POINT('Ctrl Pts',(108.042928131883,10.7592852632532,10.2036032882772));
#102903=CARTESIAN_POINT('Ctrl Pts',(108.042913268912,10.7546834567117,10.2038667980765));
#102904=CARTESIAN_POINT('Ctrl Pts',(108.042916139437,10.7500816311095,10.2041303078758));
#102905=CARTESIAN_POINT('Origin',(110.,10.75,10.13));
#102906=CARTESIAN_POINT('',(108.048535129176,10.7509086719559,11.0058696921242));
#102907=CARTESIAN_POINT('',(108.048310783185,10.7510873236897,10.9041303078758));
#102908=CARTESIAN_POINT('',(108.046,10.75,10.13));
#102909=CARTESIAN_POINT('Ctrl Pts',(108.048535129176,10.7509086719559,11.0058696921242));
#102910=CARTESIAN_POINT('Ctrl Pts',(108.047412644922,11.0114136919884,10.9910628854676));
#102911=CARTESIAN_POINT('Ctrl Pts',(108.096036433601,11.2715169252527,10.976256078811));
#102912=CARTESIAN_POINT('Ctrl Pts',(108.196425832272,11.5098122693262,10.9614492721544));
#102913=CARTESIAN_POINT('Ctrl Pts',(108.444567853022,12.0988295261007,10.9248498804526));
#102914=CARTESIAN_POINT('Ctrl Pts',(109.00898588976,12.5546055767633,10.8882504887508));
#102915=CARTESIAN_POINT('Ctrl Pts',(109.637050927409,12.6731386933476,10.851651097049));
#102916=CARTESIAN_POINT('Ctrl Pts',(110.265115965058,12.7916718099319,10.8150517053472));
#102917=CARTESIAN_POINT('Ctrl Pts',(110.956828003617,12.5729619924379,10.7784523136454));
#102918=CARTESIAN_POINT('Ctrl Pts',(111.402582247255,12.1149020121669,10.7418529219436));
#102919=CARTESIAN_POINT('Ctrl Pts',(111.848336490893,11.6568420318959,10.7052535302418));
#102920=CARTESIAN_POINT('Ctrl Pts',(112.04813293961,10.9594318888478,10.66865413854));
#102921=CARTESIAN_POINT('Ctrl Pts',(111.912544295249,10.3348268050029,10.6320547468382));
#102922=CARTESIAN_POINT('Ctrl Pts',(111.776955650888,9.71022172115799,10.5954553551364));
#102923=CARTESIAN_POINT('Ctrl Pts',(111.30598191345,9.1584216965162,10.5588559634346));
#102924=CARTESIAN_POINT('Ctrl Pts',(110.710427174364,8.92640802451273,10.5222565717328));
#102925=CARTESIAN_POINT('Ctrl Pts',(110.114872435277,8.69439435250926,10.485657180031));
#102926=CARTESIAN_POINT('Ctrl Pts',(109.394736694541,8.7821670331441,10.4490577883292));
#102927=CARTESIAN_POINT('Ctrl Pts',(108.872346970554,9.15043971407259,10.4124583966274));
#102928=CARTESIAN_POINT('Ctrl Pts',(108.365227030973,9.50794754993976,10.3769288284597));
#102929=CARTESIAN_POINT('Ctrl Pts',(108.044461584221,10.1297966663688,10.341399260292));
#102930=CARTESIAN_POINT('Ctrl Pts',(108.042985073083,10.7503289497149,10.3058696921242));
#102931=CARTESIAN_POINT('Ctrl Pts',(108.042916139437,10.7500816311095,10.2041303078758));
#102932=CARTESIAN_POINT('Ctrl Pts',(108.043311961662,10.1155268931863,10.2404661897783));
#102933=CARTESIAN_POINT('Ctrl Pts',(108.380895852216,9.48060973009477,10.2768020716808));
#102934=CARTESIAN_POINT('Ctrl Pts',(108.907340147268,9.12633446092207,10.3131379535833));
#102935=CARTESIAN_POINT('Ctrl Pts',(109.437602245088,8.76948996815607,10.3497373452851));
#102936=CARTESIAN_POINT('Ctrl Pts',(110.159473931937,8.69737258958249,10.3863367369869));
#102937=CARTESIAN_POINT('Ctrl Pts',(110.749851193771,8.94226148910796,10.4229361286887));
#102938=CARTESIAN_POINT('Ctrl Pts',(111.340228455606,9.18715038863343,10.4595355203905));
#102939=CARTESIAN_POINT('Ctrl Pts',(111.799111292426,9.74904556625794,10.4961349120923));
#102940=CARTESIAN_POINT('Ctrl Pts',(111.921107403561,10.3764472185271,10.5327343037941));
#102941=CARTESIAN_POINT('Ctrl Pts',(112.043103514695,11.0038488707963,10.5693336954959));
#102942=CARTESIAN_POINT('Ctrl Pts',(111.828212900144,11.6967569977101,10.6059330871977));
#102943=CARTESIAN_POINT('Ctrl Pts',(111.372618886398,12.145031443827,10.6425324788995));
#102944=CARTESIAN_POINT('Ctrl Pts',(110.917024872652,12.5933058899439,10.6791318706013));
#102945=CARTESIAN_POINT('Ctrl Pts',(110.220727459712,12.7969466552638,10.7157312623031));
#102946=CARTESIAN_POINT('Ctrl Pts',(109.595383820435,12.6648057561534,10.7523306540049));
#102947=CARTESIAN_POINT('Ctrl Pts',(108.970040181158,12.5326648570429,10.7889300457067));
#102948=CARTESIAN_POINT('Ctrl Pts',(108.415650315544,12.0647422935019,10.8255294374085));
#102949=CARTESIAN_POINT('Ctrl Pts',(108.180354709203,11.4704764758426,10.8621288291103));
#102950=CARTESIAN_POINT('Ctrl Pts',(108.090346260485,11.2431499005374,10.8761293220321));
#102951=CARTESIAN_POINT('Ctrl Pts',(108.047031470958,10.9973352807835,10.8901298149539));
#102952=CARTESIAN_POINT('Ctrl Pts',(108.048310783185,10.7510873236897,10.9041303078758));
#102953=CARTESIAN_POINT('Origin',(110.,10.75,10.13));
#102954=CARTESIAN_POINT('',(108.045710748453,10.7483378582515,11.7058696921242));
#102955=CARTESIAN_POINT('',(108.04612122492,10.7483233200191,11.6041303078758));
#102956=CARTESIAN_POINT('',(108.046,10.75,10.13));
#102957=CARTESIAN_POINT('Ctrl Pts',(108.045710748453,10.7483378582515,11.7058696921242));
#102958=CARTESIAN_POINT('Ctrl Pts',(108.050148979404,11.2486837218457,11.6773259023451));
#102959=CARTESIAN_POINT('Ctrl Pts',(108.246601184755,11.7521292435267,11.6487821125659));
#102960=CARTESIAN_POINT('Ctrl Pts',(108.593113995841,12.1104654471406,11.6202383227868));
#102961=CARTESIAN_POINT('Ctrl Pts',(109.037419331633,12.5699309623533,11.583638931085));
#102962=CARTESIAN_POINT('Ctrl Pts',(109.728437171546,12.7908243149632,11.5470395393832));
#102963=CARTESIAN_POINT('Ctrl Pts',(110.356873438286,12.6742753994169,11.5104401476814));
#102964=CARTESIAN_POINT('Ctrl Pts',(110.985309705026,12.5577264838707,11.4738407559796));
#102965=CARTESIAN_POINT('Ctrl Pts',(111.551164398593,12.1037353001683,11.4372413642778));
#102966=CARTESIAN_POINT('Ctrl Pts',(111.801165467383,11.5155046846917,11.400641972576));
#102967=CARTESIAN_POINT('Ctrl Pts',(112.051166536173,10.9272740692151,11.3640425808742));
#102968=CARTESIAN_POINT('Ctrl Pts',(111.985313980186,10.2048040219644,11.3274431891724));
#102969=CARTESIAN_POINT('Ctrl Pts',(111.633082878848,9.67146637800422,11.2908437974706));
#102970=CARTESIAN_POINT('Ctrl Pts',(111.28085177751,9.13812873404405,11.2542444057688));
#102971=CARTESIAN_POINT('Ctrl Pts',(110.642242130822,8.79392349337443,11.217645014067));
#102972=CARTESIAN_POINT('Ctrl Pts',(110.003090527121,8.7929141787187,11.1810456223652));
#102973=CARTESIAN_POINT('Ctrl Pts',(109.36393892342,8.79190486406298,11.1444462306634));
#102974=CARTESIAN_POINT('Ctrl Pts',(108.724245362707,9.13409147542115,11.1078468389616));
#102975=CARTESIAN_POINT('Ctrl Pts',(108.370331584732,9.66631401254336,11.0712474472598));
#102976=CARTESIAN_POINT('Ctrl Pts',(108.159598680535,9.98321832061778,11.0494548622146));
#102977=CARTESIAN_POINT('Ctrl Pts',(108.050187195968,10.3674986676641,11.0276622771694));
#102978=CARTESIAN_POINT('Ctrl Pts',(108.048535129176,10.7509086719559,11.0058696921242));
#102979=CARTESIAN_POINT('Ctrl Pts',(108.048310783185,10.7510873236897,10.9041303078758));
#102980=CARTESIAN_POINT('Ctrl Pts',(108.050375785303,10.3536061286908,10.9267292066557));
#102981=CARTESIAN_POINT('Ctrl Pts',(108.168629869771,9.95499588151061,10.9493281054357));
#102982=CARTESIAN_POINT('Ctrl Pts',(108.394243058791,9.63118813810347,10.9719270042157));
#102983=CARTESIAN_POINT('Ctrl Pts',(108.759628361785,9.10677468980156,11.0085263959175));
#102984=CARTESIAN_POINT('Ctrl Pts',(109.406600314839,8.77855686497553,11.0451257876193));
#102985=CARTESIAN_POINT('Ctrl Pts',(110.045579427837,8.79344234627983,11.0817251793211));
#102986=CARTESIAN_POINT('Ctrl Pts',(110.684558540835,8.80832782758412,11.1183245710229));
#102987=CARTESIAN_POINT('Ctrl Pts',(111.315544813776,9.16631661501872,11.1549239627247));
#102988=CARTESIAN_POINT('Ctrl Pts',(111.656113819574,9.70717578031639,11.1915233544265));
#102989=CARTESIAN_POINT('Ctrl Pts',(111.996682825373,10.2480349456141,11.2281227461283));
#102990=CARTESIAN_POINT('Ctrl Pts',(112.04683456403,10.9717644887748,11.2647221378301));
#102991=CARTESIAN_POINT('Ctrl Pts',(111.784121516993,11.5544288341185,11.3013215295319));
#102992=CARTESIAN_POINT('Ctrl Pts',(111.521408469956,12.1370931794621,11.3379209212337));
#102993=CARTESIAN_POINT('Ctrl Pts',(110.945830637226,12.5786923269888,11.3745203129355));
#102994=CARTESIAN_POINT('Ctrl Pts',(110.315012069668,12.6815700175268,11.4111197046373));
#102995=CARTESIAN_POINT('Ctrl Pts',(109.684193502111,12.7844477080649,11.4477190963391));
#102996=CARTESIAN_POINT('Ctrl Pts',(108.998134199725,12.5486039416144,11.4843184880409));
#102997=CARTESIAN_POINT('Ctrl Pts',(108.563908838614,12.0796005086416,11.5209178797427));
#102998=CARTESIAN_POINT('Ctrl Pts',(108.234823709282,11.7241582217096,11.548655355787));
#102999=CARTESIAN_POINT('Ctrl Pts',(108.050382574886,11.2347977446687,11.5763928318314));
#103000=CARTESIAN_POINT('Ctrl Pts',(108.04612122492,10.7483233200191,11.6041303078758));
#103001=CARTESIAN_POINT('Origin',(110.,10.75,10.13));
#103002=CARTESIAN_POINT('',(108.044526058825,10.7514351493348,12.4058696921242));
#103003=CARTESIAN_POINT('',(108.044157220265,10.7512978840258,12.3041303078758));
#103004=CARTESIAN_POINT('',(108.046,10.75,10.13));
#103005=CARTESIAN_POINT('Ctrl Pts',(108.044526058825,10.7514351493348,12.4058696921242));
#103006=CARTESIAN_POINT('Ctrl Pts',(108.043703950285,10.8508683356403,12.4001883109243));
#103007=CARTESIAN_POINT('Ctrl Pts',(108.05065038668,10.9501864196576,12.3945069297244));
#103008=CARTESIAN_POINT('Ctrl Pts',(108.065770181827,11.0482442275904,12.3888255485245));
#103009=CARTESIAN_POINT('Ctrl Pts',(108.163171726549,11.6799314873731,12.3522261568227));
#103010=CARTESIAN_POINT('Ctrl Pts',(108.599761238115,12.2593182797734,12.3156267651209));
#103011=CARTESIAN_POINT('Ctrl Pts',(109.18012462215,12.5270758880419,12.2790273734191));
#103012=CARTESIAN_POINT('Ctrl Pts',(109.760488006184,12.7948334963104,12.2424279817173));
#103013=CARTESIAN_POINT('Ctrl Pts',(110.484625262688,12.7509619204471,12.2058285900155));
#103014=CARTESIAN_POINT('Ctrl Pts',(111.028418379987,12.4150976327762,12.1692291983137));
#103015=CARTESIAN_POINT('Ctrl Pts',(111.572211497286,12.0792333451053,12.1326298066119));
#103016=CARTESIAN_POINT('Ctrl Pts',(111.935660475381,11.4513763456268,12.0960304149101));
#103017=CARTESIAN_POINT('Ctrl Pts',(111.956088422006,10.8125504704608,12.0594310232083));
#103018=CARTESIAN_POINT('Ctrl Pts',(111.97651636863,10.1737245952948,12.0228316315065));
#103019=CARTESIAN_POINT('Ctrl Pts',(111.653923283786,9.52392984444133,11.9862322398047));
#103020=CARTESIAN_POINT('Ctrl Pts',(111.132699274202,9.15400914676403,11.9496328481029));
#103021=CARTESIAN_POINT('Ctrl Pts',(110.611475264618,8.78408844908674,11.9130334564011));
#103022=CARTESIAN_POINT('Ctrl Pts',(109.891620330295,8.69404180458565,11.8764340646993));
#103023=CARTESIAN_POINT('Ctrl Pts',(109.295335796589,8.9241733850372,11.8398346729976));
#103024=CARTESIAN_POINT('Ctrl Pts',(108.699051262883,9.15430496548875,11.8032352812958));
#103025=CARTESIAN_POINT('Ctrl Pts',(108.226337129794,9.70461477089292,11.7666358895939));
#103026=CARTESIAN_POINT('Ctrl Pts',(108.088776479085,10.3287885125027,11.7300364978922));
#103027=CARTESIAN_POINT('Ctrl Pts',(108.058499094932,10.466170445895,11.7219808959695));
#103028=CARTESIAN_POINT('Ctrl Pts',(108.044458195024,10.6071307119006,11.7139252940469));
#103029=CARTESIAN_POINT('Ctrl Pts',(108.045710748453,10.7483378582515,11.7058696921242));
#103030=CARTESIAN_POINT('Ctrl Pts',(108.04612122492,10.7483233200191,11.6041303078758));
#103031=CARTESIAN_POINT('Ctrl Pts',(108.044759755552,10.5928983882826,11.6129922235332));
#103032=CARTESIAN_POINT('Ctrl Pts',(108.061790220506,10.4377680516706,11.6218541391906));
#103033=CARTESIAN_POINT('Ctrl Pts',(108.098371525177,10.2873938172196,11.630716054848));
#103034=CARTESIAN_POINT('Ctrl Pts',(108.249450992684,9.66635365826534,11.6673154465498));
#103035=CARTESIAN_POINT('Ctrl Pts',(108.734001347535,9.12643643985169,11.7039148382516));
#103036=CARTESIAN_POINT('Ctrl Pts',(109.335141712287,8.90930480675388,11.7405142299534));
#103037=CARTESIAN_POINT('Ctrl Pts',(109.936282077039,8.69217317365606,11.7771136216552));
#103038=CARTESIAN_POINT('Ctrl Pts',(110.654012451694,8.79782712587406,11.813713013357));
#103039=CARTESIAN_POINT('Ctrl Pts',(111.167082441064,9.1789767949659,11.8503124050588));
#103040=CARTESIAN_POINT('Ctrl Pts',(111.680152430435,9.56012646405774,11.8869117967606));
#103041=CARTESIAN_POINT('Ctrl Pts',(111.98856203452,10.2167718500234,11.9235111884624));
#103042=CARTESIAN_POINT('Ctrl Pts',(111.954269571355,10.8550037142087,11.9601105801642));
#103043=CARTESIAN_POINT('Ctrl Pts',(111.919977108191,11.493235578394,11.996709971866));
#103044=CARTESIAN_POINT('Ctrl Pts',(111.542982577776,12.113053920799,12.0333093635678));
#103045=CARTESIAN_POINT('Ctrl Pts',(110.99202572961,12.4370329850584,12.0699087552696));
#103046=CARTESIAN_POINT('Ctrl Pts',(110.441068881443,12.7610120493179,12.1065081469714));
#103047=CARTESIAN_POINT('Ctrl Pts',(109.716149715525,12.7891518354319,12.1431075386732));
#103048=CARTESIAN_POINT('Ctrl Pts',(109.141736268846,12.5088572115586,12.179706930375));
#103049=CARTESIAN_POINT('Ctrl Pts',(108.567322822166,12.2285625876853,12.2163063220768));
#103050=CARTESIAN_POINT('Ctrl Pts',(108.143415094725,11.6398335538247,12.2529057137786));
#103051=CARTESIAN_POINT('Ctrl Pts',(108.059750815919,11.0061805088822,12.2895051054804));
#103052=CARTESIAN_POINT('Ctrl Pts',(108.048606668854,10.9217774300347,12.2943801729455));
#103053=CARTESIAN_POINT('Ctrl Pts',(108.043499273272,10.8365772892847,12.2992552404106));
#103054=CARTESIAN_POINT('Ctrl Pts',(108.044157220265,10.7512978840258,12.3041303078758));
#103055=CARTESIAN_POINT('Origin',(110.,10.75,10.13));
#103056=CARTESIAN_POINT('',(108.048941223895,10.7496876406009,13.1058696921242));
#103057=CARTESIAN_POINT('',(108.048980644574,10.7499134704375,13.0041303078758));
#103058=CARTESIAN_POINT('',(108.046,10.75,10.13));
#103059=CARTESIAN_POINT('Ctrl Pts',(108.048941223895,10.7496876406009,13.1058696921242));
#103060=CARTESIAN_POINT('Ctrl Pts',(108.049427891664,11.0915066401091,13.0864513278018));
#103061=CARTESIAN_POINT('Ctrl Pts',(108.135074391136,11.4335566218935,13.0670329634793));
#103062=CARTESIAN_POINT('Ctrl Pts',(108.304422957909,11.7273573425776,13.0476145991569));
#103063=CARTESIAN_POINT('Ctrl Pts',(108.62360815943,12.2811077759316,13.0110152074551));
#103064=CARTESIAN_POINT('Ctrl Pts',(109.240136984181,12.6634573039523,12.9744158157533));
#103065=CARTESIAN_POINT('Ctrl Pts',(109.878048356021,12.7032830865787,12.9378164240515));
#103066=CARTESIAN_POINT('Ctrl Pts',(110.515959727861,12.7431088692051,12.9012170323497));
#103067=CARTESIAN_POINT('Ctrl Pts',(111.17525364679,12.4404109064371,12.8646176406479));
#103068=CARTESIAN_POINT('Ctrl Pts',(111.56083918769,11.9306676298148,12.8280182489461));
#103069=CARTESIAN_POINT('Ctrl Pts',(111.94642472859,11.4209243531925,12.7914188572443));
#103070=CARTESIAN_POINT('Ctrl Pts',(112.05830189146,10.7041357627159,12.7548194655425));
#103071=CARTESIAN_POINT('Ctrl Pts',(111.846393492449,10.1011340438354,12.7182200738407));
#103072=CARTESIAN_POINT('Ctrl Pts',(111.634485093438,9.49813232495484,12.6816206821389));
#103073=CARTESIAN_POINT('Ctrl Pts',(111.098791132546,9.00891747767032,12.6450212904371));
#103074=CARTESIAN_POINT('Ctrl Pts',(110.479084870382,8.85245653454336,12.6084218987353));
#103075=CARTESIAN_POINT('Ctrl Pts',(109.859378608218,8.69599559141641,12.5718225070335));
#103076=CARTESIAN_POINT('Ctrl Pts',(109.155660044781,8.872288552447,12.5352231153317));
#103077=CARTESIAN_POINT('Ctrl Pts',(108.682907552003,9.30242889654483,12.4986237236299));
#103078=CARTESIAN_POINT('Ctrl Pts',(108.283541173031,9.66579787776891,12.467705713128));
#103079=CARTESIAN_POINT('Ctrl Pts',(108.048999963953,10.2103209043556,12.4367877026261));
#103080=CARTESIAN_POINT('Ctrl Pts',(108.044526058825,10.7514351493348,12.4058696921242));
#103081=CARTESIAN_POINT('Ctrl Pts',(108.044157220265,10.7512978840258,12.3041303078758));
#103082=CARTESIAN_POINT('Ctrl Pts',(108.048438786391,10.1963452556777,12.3358546321124));
#103083=CARTESIAN_POINT('Ctrl Pts',(108.296865792646,9.63803600659926,12.3675789563491));
#103084=CARTESIAN_POINT('Ctrl Pts',(108.714645515603,9.27417507348757,12.3993032805858));
#103085=CARTESIAN_POINT('Ctrl Pts',(109.196625324267,8.85439973906008,12.4359026722876));
#103086=CARTESIAN_POINT('Ctrl Pts',(109.904005771767,8.69342612622964,12.4725020639894));
#103087=CARTESIAN_POINT('Ctrl Pts',(110.520169044345,8.86330463874869,12.5091014556912));
#103088=CARTESIAN_POINT('Ctrl Pts',(111.136332316922,9.03318315126774,12.545700847393));
#103089=CARTESIAN_POINT('Ctrl Pts',(111.661278414578,9.53391378913629,12.5823002390948));
#103090=CARTESIAN_POINT('Ctrl Pts',(111.860045572213,10.1413737179372,12.6188996307966));
#103091=CARTESIAN_POINT('Ctrl Pts',(112.058812729848,10.7488336467382,12.6554990224984));
#103092=CARTESIAN_POINT('Ctrl Pts',(111.931400947464,11.4630228664716,12.6920984142002));
#103093=CARTESIAN_POINT('Ctrl Pts',(111.534838876806,11.9642755498955,12.728697805902));
#103094=CARTESIAN_POINT('Ctrl Pts',(111.138276806148,12.4655282333194,12.7652971976038));
#103095=CARTESIAN_POINT('Ctrl Pts',(110.472564447218,12.7538443804338,12.8018965893056));
#103096=CARTESIAN_POINT('Ctrl Pts',(109.835669034371,12.7001768448261,12.8384959810074));
#103097=CARTESIAN_POINT('Ctrl Pts',(109.198773621524,12.6465093092184,12.8750953727092));
#103098=CARTESIAN_POINT('Ctrl Pts',(108.59069515476,12.2508580908886,12.911694764411));
#103099=CARTESIAN_POINT('Ctrl Pts',(108.283605344712,11.6903117653571,12.9482941561128));
#103100=CARTESIAN_POINT('Ctrl Pts',(108.12743960496,11.4052546624268,12.9669062067004));
#103101=CARTESIAN_POINT('Ctrl Pts',(108.049111717213,11.0775544875257,12.9855182572881));
#103102=CARTESIAN_POINT('Ctrl Pts',(108.048980644574,10.7499134704375,13.0041303078758));
#103103=CARTESIAN_POINT('Origin',(110.,10.75,10.13));
#103104=CARTESIAN_POINT('',(108.04401647614,10.7486495636155,13.8058696921242));
#103105=CARTESIAN_POINT('',(108.043923528227,10.7487415210877,13.7041303078758));
#103106=CARTESIAN_POINT('',(108.046,10.75,10.13));
#103107=CARTESIAN_POINT('Ctrl Pts',(108.04401647614,10.7486495636155,13.8058696921242));
#103108=CARTESIAN_POINT('Ctrl Pts',(108.04772980719,11.3276092745096,13.7727143446792));
#103109=CARTESIAN_POINT('Ctrl Pts',(108.321504296629,11.911076308,13.7395589972342));
#103110=CARTESIAN_POINT('Ctrl Pts',(108.772311391298,12.2745082768577,13.7064036497892));
#103111=CARTESIAN_POINT('Ctrl Pts',(109.269946515379,12.6756920981778,13.6698042580874));
#103112=CARTESIAN_POINT('Ctrl Pts',(109.983303336603,12.8087539116218,13.6332048663856));
#103113=CARTESIAN_POINT('Ctrl Pts',(110.592540776308,12.6151257353379,13.5966054746838));
#103114=CARTESIAN_POINT('Ctrl Pts',(111.201778216014,12.421497559054,13.560006082982));
#103115=CARTESIAN_POINT('Ctrl Pts',(111.706896274201,11.9011793930423,13.5234066912802));
#103116=CARTESIAN_POINT('Ctrl Pts',(111.882075975322,11.2865802792359,13.4868072995784));
#103117=CARTESIAN_POINT('Ctrl Pts',(112.057255676443,10.6719811654296,13.4502079078766));
#103118=CARTESIAN_POINT('Ctrl Pts',(111.902497020499,9.96310110382854,13.4136085161748));
#103119=CARTESIAN_POINT('Ctrl Pts',(111.486937042034,9.47746498726815,13.377009124473));
#103120=CARTESIAN_POINT('Ctrl Pts',(111.071377063569,8.99182887070775,13.3404097327712));
#103121=CARTESIAN_POINT('Ctrl Pts',(110.395015762583,8.72943669918797,13.3038103410694));
#103122=CARTESIAN_POINT('Ctrl Pts',(109.760651801791,8.80761723079152,13.2672109493676));
#103123=CARTESIAN_POINT('Ctrl Pts',(109.126287841,8.88579776239506,13.2306115576658));
#103124=CARTESIAN_POINT('Ctrl Pts',(108.533921220403,9.30455099712193,13.194012165964));
#103125=CARTESIAN_POINT('Ctrl Pts',(108.24865869925,9.87650328382905,13.1574127742622));
#103126=CARTESIAN_POINT('Ctrl Pts',(108.114746550486,10.1449975795173,13.1402317468829));
#103127=CARTESIAN_POINT('Ctrl Pts',(108.048510628808,10.4472521989845,13.1230507195036));
#103128=CARTESIAN_POINT('Ctrl Pts',(108.048941223895,10.7496876406009,13.1058696921242));
#103129=CARTESIAN_POINT('Ctrl Pts',(108.048980644574,10.7499134704375,13.0041303078758));
#103130=CARTESIAN_POINT('Ctrl Pts',(108.04885397136,10.433269653595,13.0221176489899));
#103131=CARTESIAN_POINT('Ctrl Pts',(108.121762890827,10.1166810899737,13.040104990104));
#103132=CARTESIAN_POINT('Ctrl Pts',(108.268031420165,9.83869284548097,13.0580923312181));
#103133=CARTESIAN_POINT('Ctrl Pts',(108.565648458999,9.27306168386946,13.0946917229199));
#103134=CARTESIAN_POINT('Ctrl Pts',(109.16698369,8.86724079337956,13.1312911146217));
#103135=CARTESIAN_POINT('Ctrl Pts',(109.802886885463,8.80286509693592,13.1678905063235));
#103136=CARTESIAN_POINT('Ctrl Pts',(110.438790080927,8.73848940049229,13.2044898980253));
#103137=CARTESIAN_POINT('Ctrl Pts',(111.109261240853,9.01555889809494,13.2410892897271));
#103138=CARTESIAN_POINT('Ctrl Pts',(111.514197467183,9.51007429098298,13.2776886814289));
#103139=CARTESIAN_POINT('Ctrl Pts',(111.919133693514,10.004589683871,13.3142880731307));
#103140=CARTESIAN_POINT('Ctrl Pts',(112.058534986249,10.7165509720445,13.3508874648325));
#103141=CARTESIAN_POINT('Ctrl Pts',(111.870017324534,11.3272598408929,13.3874868565343));
#103142=CARTESIAN_POINT('Ctrl Pts',(111.68149966282,11.9379687097414,13.4240862482361));
#103143=CARTESIAN_POINT('Ctrl Pts',(111.165063046655,12.447425159265,13.4606856399379));
#103144=CARTESIAN_POINT('Ctrl Pts',(110.551838236876,12.6276618241303,13.4972850316397));
#103145=CARTESIAN_POINT('Ctrl Pts',(109.938613427096,12.8078984889955,13.5338844233415));
#103146=CARTESIAN_POINT('Ctrl Pts',(109.228600423702,12.6589153692025,13.5704838150433));
#103147=CARTESIAN_POINT('Ctrl Pts',(108.739640464735,12.2472714195058,13.6070832067451));
#103148=CARTESIAN_POINT('Ctrl Pts',(108.307464369448,11.8834324761199,13.6394322404553));
#103149=CARTESIAN_POINT('Ctrl Pts',(108.047979944815,11.3143969128506,13.6717812741655));
#103150=CARTESIAN_POINT('Ctrl Pts',(108.043923528227,10.7487415210877,13.7041303078758));
#103151=CARTESIAN_POINT('Origin',(110.,10.75,5.2859437743963));
#103152=CARTESIAN_POINT('',(108.446841388827,10.7497513433749,13.3359437743963));
#103153=CARTESIAN_POINT('',(108.442847005198,10.7489981760756,13.4740562256037));
#103154=CARTESIAN_POINT('',(108.4445,10.7499999999999,5.2859437743963));
#103155=CARTESIAN_POINT('',(109.142424689894,12.0477460604818,13.926));
#103156=CARTESIAN_POINT('Ctrl Pts',(108.446841388827,10.7497513433749,13.3359437743963));
#103157=CARTESIAN_POINT('Ctrl Pts',(108.446498609576,10.508994777646,13.3531248017756));
#103158=CARTESIAN_POINT('Ctrl Pts',(108.611548063658,9.7558240105893,13.4069052208568));
#103159=CARTESIAN_POINT('Ctrl Pts',(109.77603224924,8.93263191544926,13.4972850316397));
#103160=CARTESIAN_POINT('Ctrl Pts',(111.391303493381,9.55927115209057,13.6070832067451));
#103161=CARTESIAN_POINT('Ctrl Pts',(111.760894725706,11.2522029880481,13.7168813818505));
#103162=CARTESIAN_POINT('Ctrl Pts',(110.592954496938,12.4552890943434,13.8231869796021));
#103163=CARTESIAN_POINT('Ctrl Pts',(109.526460624714,12.3008132614142,13.892893185652));
#103164=CARTESIAN_POINT('Ctrl Pts',(109.140566776777,12.049156215532,13.926));
#103165=CARTESIAN_POINT('',(110.948473540785,11.982873956425,13.926));
#103166=CARTESIAN_POINT('Origin',(110.,10.75,13.926));
#103167=CARTESIAN_POINT('Ctrl Pts',(108.442847005198,10.7489981760756,13.4740562256037));
#103168=CARTESIAN_POINT('Ctrl Pts',(108.442422725546,10.6898336234053,13.4783065835953));
#103169=CARTESIAN_POINT('Ctrl Pts',(108.472082002041,10.1216556996131,13.5191563332887));
#103170=CARTESIAN_POINT('Ctrl Pts',(109.169225983483,9.11850985467691,13.5966054746838));
#103171=CARTESIAN_POINT('Ctrl Pts',(110.901845461742,9.15519245562723,13.7064036497892));
#103172=CARTESIAN_POINT('Ctrl Pts',(111.825924765157,10.6229447474917,13.8162018248946));
#103173=CARTESIAN_POINT('Ctrl Pts',(111.353491586843,11.6712858186231,13.8894006082982));
#103174=CARTESIAN_POINT('Ctrl Pts',(110.948473540785,11.982873956425,13.926));
#103175=CARTESIAN_POINT('Origin',(110.,10.75,5.2859437743963));
#103176=CARTESIAN_POINT('',(108.443326655324,10.7511424640687,12.6359437743963));
#103177=CARTESIAN_POINT('',(108.446872770028,10.7499311173313,12.7740562256037));
#103178=CARTESIAN_POINT('',(108.4445,10.7499999999999,5.2859437743963));
#103179=CARTESIAN_POINT('Ctrl Pts',(108.443326655324,10.7511424640687,12.6359437743963));
#103180=CARTESIAN_POINT('Ctrl Pts',(108.446888149401,10.3203834015993,12.6668617848982));
#103181=CARTESIAN_POINT('Ctrl Pts',(108.854614518196,9.37378473252757,12.7343791871019));
#103182=CARTESIAN_POINT('Ctrl Pts',(110.448258777128,8.97455089128206,12.8384959810074));
#103183=CARTESIAN_POINT('Ctrl Pts',(111.727591360803,10.1428830739091,12.9482941561128));
#103184=CARTESIAN_POINT('Ctrl Pts',(111.460408770971,11.8547018853006,13.0580923312181));
#103185=CARTESIAN_POINT('Ctrl Pts',(109.885897474817,12.5775985297513,13.1678905063236));
#103186=CARTESIAN_POINT('Ctrl Pts',(108.643912399514,11.8073629977093,13.2605076540496));
#103187=CARTESIAN_POINT('Ctrl Pts',(108.447228805263,11.0218595592065,13.3165254100738));
#103188=CARTESIAN_POINT('Ctrl Pts',(108.446841388827,10.7497513433749,13.3359437743963));
#103189=CARTESIAN_POINT('Ctrl Pts',(108.446872770028,10.7499311173313,12.7740562256037));
#103190=CARTESIAN_POINT('Ctrl Pts',(108.446771930629,10.4978638414365,12.7920435667178));
#103191=CARTESIAN_POINT('Ctrl Pts',(108.622907167769,9.7330410716517,12.8466302995338));
#103192=CARTESIAN_POINT('Ctrl Pts',(109.815568107276,8.92815438021742,12.9378164240515));
#103193=CARTESIAN_POINT('Ctrl Pts',(111.416772645554,9.58984568552079,13.0476145991569));
#103194=CARTESIAN_POINT('Ctrl Pts',(111.749687759447,11.2901360392881,13.1574127742623));
#103195=CARTESIAN_POINT('Ctrl Pts',(110.516345144641,12.5068087730147,13.2672109493676));
#103196=CARTESIAN_POINT('Ctrl Pts',(108.886346860443,12.1647837277323,13.3727587664815));
#103197=CARTESIAN_POINT('Ctrl Pts',(108.446076153613,11.1992934482799,13.4417071918935));
#103198=CARTESIAN_POINT('Ctrl Pts',(108.442847005198,10.7489981760756,13.4740562256037));
#103199=CARTESIAN_POINT('Origin',(110.,10.75,5.2859437743963));
#103200=CARTESIAN_POINT('',(108.444269738597,10.7486768364944,11.9359437743963));
#103201=CARTESIAN_POINT('',(108.443033037933,10.7510331927338,12.0740562256037));
#103202=CARTESIAN_POINT('',(108.4445,10.7499999999999,5.2859437743963));
#103203=CARTESIAN_POINT('Ctrl Pts',(108.444269738597,10.7486768364944,11.9359437743963));
#103204=CARTESIAN_POINT('Ctrl Pts',(108.443272631709,10.6362675651798,11.9439993763189));
#103205=CARTESIAN_POINT('Ctrl Pts',(108.505232777979,10.0142334536265,11.9886543699434));
#103206=CARTESIAN_POINT('Ctrl Pts',(109.340676086711,9.04165274898235,12.0699087552696));
#103207=CARTESIAN_POINT('Ctrl Pts',(111.059817873312,9.25670017301735,12.179706930375));
#103208=CARTESIAN_POINT('Ctrl Pts',(111.830227612529,10.8085257640398,12.2895051054804));
#103209=CARTESIAN_POINT('Ctrl Pts',(110.962246723952,12.3079600977483,12.3993032805858));
#103210=CARTESIAN_POINT('Ctrl Pts',(109.232877989319,12.4127332342713,12.5091014556912));
#103211=CARTESIAN_POINT('Ctrl Pts',(108.483824735014,11.4186837877046,12.5879816202947));
#103212=CARTESIAN_POINT('Ctrl Pts',(108.442672208121,10.8302971832592,12.6302623931964));
#103213=CARTESIAN_POINT('Ctrl Pts',(108.443326655324,10.7511424640687,12.6359437743963));
#103214=CARTESIAN_POINT('Ctrl Pts',(108.443033037933,10.7510331927338,12.0740562256037));
#103215=CARTESIAN_POINT('Ctrl Pts',(108.446441418747,10.3092579555816,12.1057805498404));
#103216=CARTESIAN_POINT('Ctrl Pts',(108.872356835445,9.35206525720305,12.1741042657789));
#103217=CARTESIAN_POINT('Ctrl Pts',(110.486699725726,8.98470055506267,12.2790273734191));
#103218=CARTESIAN_POINT('Ctrl Pts',(111.74036449784,10.1805344965231,12.3888255485245));
#103219=CARTESIAN_POINT('Ctrl Pts',(111.436082469949,11.8861455476417,12.4986237236299));
#103220=CARTESIAN_POINT('Ctrl Pts',(109.846242795973,12.5746958549649,12.6084218987353));
#103221=CARTESIAN_POINT('Ctrl Pts',(108.63194517067,11.7846031923792,12.7002327327266));
#103222=CARTESIAN_POINT('Ctrl Pts',(108.44697711163,11.010752817475,12.755444175016));
#103223=CARTESIAN_POINT('Ctrl Pts',(108.446872770028,10.7499311173313,12.7740562256037));
#103224=CARTESIAN_POINT('Origin',(110.,10.75,5.2859437743963));
#103225=CARTESIAN_POINT('',(108.446518113323,10.7507233568205,11.2359437743963));
#103226=CARTESIAN_POINT('',(108.444596502233,10.7486652631983,11.3740562256037));
#103227=CARTESIAN_POINT('',(108.4445,10.7499999999999,5.2859437743963));
#103228=CARTESIAN_POINT('Ctrl Pts',(108.446518113323,10.7507233568205,11.2359437743963));
#103229=CARTESIAN_POINT('Ctrl Pts',(108.447833256565,10.4455062321144,11.2577363594415));
#103230=CARTESIAN_POINT('Ctrl Pts',(108.68120743127,9.62583808482625,11.3161283361885));
#103231=CARTESIAN_POINT('Ctrl Pts',(110.002891673014,8.91883917199709,11.4111197046373));
#103232=CARTESIAN_POINT('Ctrl Pts',(111.528005243266,9.74086258836599,11.5209178797427));
#103233=CARTESIAN_POINT('Ctrl Pts',(111.685272875053,11.4662497303801,11.630716054848));
#103234=CARTESIAN_POINT('Ctrl Pts',(110.333911090238,12.5504615311719,11.7405142299534));
#103235=CARTESIAN_POINT('Ctrl Pts',(108.80471363849,12.061632542384,11.8422568031362));
#103236=CARTESIAN_POINT('Ctrl Pts',(108.447802833911,11.1469818471499,11.9073999846171));
#103237=CARTESIAN_POINT('Ctrl Pts',(108.444269738597,10.7486768364944,11.9359437743963));
#103238=CARTESIAN_POINT('Ctrl Pts',(108.444596502233,10.7486652631983,11.3740562256037));
#103239=CARTESIAN_POINT('Ctrl Pts',(108.443512691792,10.6249377906722,11.3829181412611));
#103240=CARTESIAN_POINT('Ctrl Pts',(108.513060951864,9.99142337839694,11.4283794486203));
#103241=CARTESIAN_POINT('Ctrl Pts',(109.377920764104,9.02774086435358,11.5104401476814));
#103242=CARTESIAN_POINT('Ctrl Pts',(111.091988723841,9.28006131881894,11.6202383227868));
#103243=CARTESIAN_POINT('Ctrl Pts',(111.82852578498,10.8482474465615,11.7300364978922));
#103244=CARTESIAN_POINT('Ctrl Pts',(110.928195705052,12.3284840355239,11.8398346729976));
#103245=CARTESIAN_POINT('Ctrl Pts',(109.196959631481,12.3956868563535,11.9496328481029));
#103246=CARTESIAN_POINT('Ctrl Pts',(108.477098834361,11.3959340229695,12.0277066989717));
#103247=CARTESIAN_POINT('Ctrl Pts',(108.442509273068,10.8189206619663,12.0691811581386));
#103248=CARTESIAN_POINT('Ctrl Pts',(108.443033037933,10.7510331927338,12.0740562256037));
#103249=CARTESIAN_POINT('Origin',(110.,10.75,5.2859437743963));
#103250=CARTESIAN_POINT('',(108.442099939192,10.7502618635012,10.5359437743963));
#103251=CARTESIAN_POINT('',(108.446339520596,10.7508655742063,10.6740562256037));
#103252=CARTESIAN_POINT('',(108.4445,10.7499999999999,5.2859437743963));
#103253=CARTESIAN_POINT('Ctrl Pts',(108.442099939192,10.7502618635012,10.5359437743963));
#103254=CARTESIAN_POINT('Ctrl Pts',(108.443275329712,10.2562813278079,10.571473342564));
#103255=CARTESIAN_POINT('Ctrl Pts',(108.961660747072,9.2513179908291,10.6436023024336));
#103256=CARTESIAN_POINT('Ctrl Pts',(110.664716078704,9.04374360829103,10.7523306540049));
#103257=CARTESIAN_POINT('Ctrl Pts',(111.789485242344,10.3615403406303,10.8621288291103));
#103258=CARTESIAN_POINT('Ctrl Pts',(111.312335739819,12.0270799683344,10.9719270042157));
#103259=CARTESIAN_POINT('Ctrl Pts',(109.660404200444,12.5493979639002,11.0817251793211));
#103260=CARTESIAN_POINT('Ctrl Pts',(108.580008787355,11.67696242414,11.1697307693813));
#103261=CARTESIAN_POINT('Ctrl Pts',(108.44562454922,10.9581008177522,11.2211369677397));
#103262=CARTESIAN_POINT('Ctrl Pts',(108.446518113323,10.7507233568205,11.2359437743963));
#103263=CARTESIAN_POINT('Ctrl Pts',(108.446339520596,10.7508655742063,10.6740562256037));
#103264=CARTESIAN_POINT('Ctrl Pts',(108.447983384872,10.4344469463554,10.6966551243837));
#103265=CARTESIAN_POINT('Ctrl Pts',(108.694577946579,9.60322729218201,10.7558534148655));
#103266=CARTESIAN_POINT('Ctrl Pts',(110.042646705583,8.91933335565637,10.851651097049));
#103267=CARTESIAN_POINT('Ctrl Pts',(111.549554301631,9.77427433649753,10.9614492721544));
#103268=CARTESIAN_POINT('Ctrl Pts',(111.669325585378,11.5026693790562,11.0712474472598));
#103269=CARTESIAN_POINT('Ctrl Pts',(110.294743212587,12.5572867904855,11.1810456223652));
#103270=CARTESIAN_POINT('Ctrl Pts',(108.788550810402,12.0395092632441,11.2819818818132));
#103271=CARTESIAN_POINT('Ctrl Pts',(108.447988789783,11.1359277849703,11.3463187495593));
#103272=CARTESIAN_POINT('Ctrl Pts',(108.444596502233,10.7486652631983,11.3740562256037));
#103273=CARTESIAN_POINT('Origin',(110.,10.75,5.2859437743963));
#103274=CARTESIAN_POINT('',(108.445976253612,10.7489330703828,9.8359437743963));
#103275=CARTESIAN_POINT('',(108.442045063917,10.7500649832092,9.97405622560371));
#103276=CARTESIAN_POINT('',(108.4445,10.7499999999999,5.2859437743963));
#103277=CARTESIAN_POINT('Ctrl Pts',(108.445976253612,10.7489330703828,9.8359437743963));
#103278=CARTESIAN_POINT('Ctrl Pts',(108.444822676107,10.571678333824,9.84861093398479));
#103279=CARTESIAN_POINT('Ctrl Pts',(108.55398870796,9.88365650751954,9.89787748527507));
#103280=CARTESIAN_POINT('Ctrl Pts',(109.557350442899,8.97314330652884,9.98374342826716));
#103281=CARTESIAN_POINT('Ctrl Pts',(111.236618208315,9.39946908721214,10.0935416033726));
#103282=CARTESIAN_POINT('Ctrl Pts',(111.808885064222,11.0347686147797,10.2033397784779));
#103283=CARTESIAN_POINT('Ctrl Pts',(110.761866842631,12.4151478173515,10.3131379535833));
#103284=CARTESIAN_POINT('Ctrl Pts',(109.032837566985,12.3049132347807,10.4229361286887));
#103285=CARTESIAN_POINT('Ctrl Pts',(108.44893261916,11.288831373407,10.4972047356264));
#103286=CARTESIAN_POINT('Ctrl Pts',(108.442064547249,10.7651360100137,10.5348739508622));
#103287=CARTESIAN_POINT('Ctrl Pts',(108.442099939192,10.7502618635012,10.5359437743963));
#103288=CARTESIAN_POINT('Ctrl Pts',(108.442045063917,10.7500649832092,9.97405622560371));
#103289=CARTESIAN_POINT('Ctrl Pts',(108.442360161907,10.2449217412237,10.0103921075062));
#103290=CARTESIAN_POINT('Ctrl Pts',(108.98178269135,9.23039281468085,10.0833273811105));
#103291=CARTESIAN_POINT('Ctrl Pts',(110.701603433992,9.05857701162966,10.1928620464167));
#103292=CARTESIAN_POINT('Ctrl Pts',(111.797497373615,10.4004827672002,10.3026602215221));
#103293=CARTESIAN_POINT('Ctrl Pts',(111.284300314861,12.0552707785837,10.4124583966274));
#103294=CARTESIAN_POINT('Ctrl Pts',(109.621418084829,12.5416011938169,10.5222565717329));
#103295=CARTESIAN_POINT('Ctrl Pts',(108.569941145921,11.654121434041,10.6094558480583));
#103296=CARTESIAN_POINT('Ctrl Pts',(108.445321112116,10.9468935666625,10.6600557326819));
#103297=CARTESIAN_POINT('Ctrl Pts',(108.446339520596,10.7508655742063,10.6740562256037));
#103298=CARTESIAN_POINT('Origin',(110.,10.75,5.2859437743963));
#103299=CARTESIAN_POINT('',(108.445121586218,10.7512991519358,9.1359437743963));
#103300=CARTESIAN_POINT('',(108.446205554653,10.7490493704098,9.2740562256037));
#103301=CARTESIAN_POINT('',(108.4445,10.7499999999999,5.2859437743963));
#103302=CARTESIAN_POINT('Ctrl Pts',(108.445121586218,10.7512991519358,9.1359437743963));
#103303=CARTESIAN_POINT('Ctrl Pts',(108.448172895975,10.3823342510321,9.16234791710734));
#103304=CARTESIAN_POINT('Ctrl Pts',(108.762681159919,9.49725890698745,9.22535145152017));
#103305=CARTESIAN_POINT('Ctrl Pts',(110.229678498517,8.93329800817414,9.32495437763481));
#103306=CARTESIAN_POINT('Ctrl Pts',(111.641231584828,9.93789334168282,9.4347525527402));
#103307=CARTESIAN_POINT('Ctrl Pts',(111.583580316096,11.6694736113398,9.5445507278456));
#103308=CARTESIAN_POINT('Ctrl Pts',(110.108333189259,12.577955759768,9.65434890295098));
#103309=CARTESIAN_POINT('Ctrl Pts',(108.717491883739,11.9340542572433,9.75147991846789));
#103310=CARTESIAN_POINT('Ctrl Pts',(108.448155722847,11.0838227880714,9.81201154228299));
#103311=CARTESIAN_POINT('Ctrl Pts',(108.445976253612,10.7489330703828,9.8359437743963));
#103312=CARTESIAN_POINT('Ctrl Pts',(108.446205554653,10.7490493704098,9.2740562256037));
#103313=CARTESIAN_POINT('Ctrl Pts',(108.445123112026,10.5604414071891,9.28752969892698));
#103314=CARTESIAN_POINT('Ctrl Pts',(108.563532910115,9.86081023996671,9.33760256395205));
#103315=CARTESIAN_POINT('Ctrl Pts',(109.596031461916,8.9639517015356,9.42427482067892));
#103316=CARTESIAN_POINT('Ctrl Pts',(111.265647793446,9.42663505898133,9.53407299578432));
#103317=CARTESIAN_POINT('Ctrl Pts',(111.802276393556,11.073973618372,9.6438711708897));
#103318=CARTESIAN_POINT('Ctrl Pts',(110.725535892815,12.4312961584497,9.7536693459951));
#103319=CARTESIAN_POINT('Ctrl Pts',(108.99930722521,12.2835491758203,9.86346752110049));
#103320=CARTESIAN_POINT('Ctrl Pts',(108.443697953399,11.266196081649,9.93692981430336));
#103321=CARTESIAN_POINT('Ctrl Pts',(108.442042778809,10.7537283095778,9.97379271580443));
#103322=CARTESIAN_POINT('Ctrl Pts',(108.442045063917,10.7500649832092,9.97405622560371));
#103323=CARTESIAN_POINT('Origin',(110.,10.75,5.2859437743963));
#103324=CARTESIAN_POINT('',(108.442605213692,10.749194935846,8.4359437743963));
#103325=CARTESIAN_POINT('',(108.444807264591,10.7513287041109,8.5740562256037));
#103326=CARTESIAN_POINT('',(108.4445,10.7499999999999,5.2859437743963));
#103327=CARTESIAN_POINT('Ctrl Pts',(108.442605213692,10.749194935846,8.4359437743963));
#103328=CARTESIAN_POINT('Ctrl Pts',(108.442290979397,10.6999103733631,8.43948550852809));
#103329=CARTESIAN_POINT('Ctrl Pts',(108.466566776117,10.1416447851508,8.47962663436168));
#103330=CARTESIAN_POINT('Ctrl Pts',(109.138403361389,9.13420003397936,8.55636715189706));
#103331=CARTESIAN_POINT('Ctrl Pts',(110.870935822764,9.13921474264243,8.66616532700245));
#103332=CARTESIAN_POINT('Ctrl Pts',(111.823820425147,10.5861787581841,8.77596350210785));
#103333=CARTESIAN_POINT('Ctrl Pts',(111.144050049243,12.179792928921,8.88576167721324));
#103334=CARTESIAN_POINT('Ctrl Pts',(109.440144306221,12.4934792638734,8.99555985231863));
#103335=CARTESIAN_POINT('Ctrl Pts',(108.526644069975,11.5463195852755,9.07895388471298));
#103336=CARTESIAN_POINT('Ctrl Pts',(108.443943405087,10.8937650170363,9.12574852540554));
#103337=CARTESIAN_POINT('Ctrl Pts',(108.445121586218,10.7512991519358,9.1359437743963));
#103338=CARTESIAN_POINT('Ctrl Pts',(108.444807264591,10.7513287041109,8.5740562256037));
#103339=CARTESIAN_POINT('Ctrl Pts',(108.448079287351,10.3712924955763,8.60126668204952));
#103340=CARTESIAN_POINT('Ctrl Pts',(108.778198422012,9.47499754635645,8.66507653019715));
#103341=CARTESIAN_POINT('Ctrl Pts',(110.269066191156,8.93871247704089,8.76548577004656));
#103342=CARTESIAN_POINT('Ctrl Pts',(111.658476300169,9.97371689050704,8.87528394515196));
#103343=CARTESIAN_POINT('Ctrl Pts',(111.563244859267,11.7036375693259,8.98508212025735));
#103344=CARTESIAN_POINT('Ctrl Pts',(110.068621537362,12.5798770967034,9.09488029536274));
#103345=CARTESIAN_POINT('Ctrl Pts',(108.703514451318,11.9115258327128,9.19120499714486));
#103346=CARTESIAN_POINT('Ctrl Pts',(108.448063463097,11.0727767611375,9.25093030722518));
#103347=CARTESIAN_POINT('Ctrl Pts',(108.446205554653,10.7490493704098,9.2740562256037));
#103348=CARTESIAN_POINT('Origin',(110.,10.75,5.2859437743963));
#103349=CARTESIAN_POINT('',(108.446844740062,10.7497785244693,7.7359437743963));
#103350=CARTESIAN_POINT('',(108.442854064965,10.7490502583051,7.8740562256037));
#103351=CARTESIAN_POINT('',(108.4445,10.7499999999999,5.2859437743963));
#103352=CARTESIAN_POINT('Ctrl Pts',(108.446844740062,10.7497785244693,7.7359437743963));
#103353=CARTESIAN_POINT('Ctrl Pts',(108.446528563922,10.5076526407742,7.75322249165064));
#103354=CARTESIAN_POINT('Ctrl Pts',(108.612900212043,9.75307183152967,7.80710060060678));
#103355=CARTESIAN_POINT('Ctrl Pts',(109.780842261901,8.93199962740631,7.8975781012647));
#103356=CARTESIAN_POINT('Ctrl Pts',(111.394373478833,9.56303689824699,8.0073762763701));
#103357=CARTESIAN_POINT('Ctrl Pts',(111.759684322617,11.256625962536,8.11717445147549));
#103358=CARTESIAN_POINT('Ctrl Pts',(110.549753543119,12.4966908797639,8.22697262658089));
#103359=CARTESIAN_POINT('Ctrl Pts',(108.902595277997,12.1835827892781,8.33322906755448));
#103360=CARTESIAN_POINT('Ctrl Pts',(108.445538197739,11.2092046738507,8.40288611682629));
#103361=CARTESIAN_POINT('Ctrl Pts',(108.442605213692,10.749194935846,8.4359437743963));
#103362=CARTESIAN_POINT('Ctrl Pts',(108.442854064965,10.7490502583051,7.8740562256037));
#103363=CARTESIAN_POINT('Ctrl Pts',(108.442415170989,10.6885200197988,7.87840427347028));
#103364=CARTESIAN_POINT('Ctrl Pts',(108.472848633662,10.1189256629246,7.91935171303865));
#103365=CARTESIAN_POINT('Ctrl Pts',(109.173686477906,9.11587493853038,7.99689854430882));
#103366=CARTESIAN_POINT('Ctrl Pts',(110.90570183064,9.15850278599423,8.10669671941421));
#103367=CARTESIAN_POINT('Ctrl Pts',(111.8269474297,10.6258137189513,8.2164948945196));
#103368=CARTESIAN_POINT('Ctrl Pts',(111.112738765821,12.2042941592694,8.32629306962499));
#103369=CARTESIAN_POINT('Ctrl Pts',(109.402424116335,12.4809136837355,8.43609124473039));
#103370=CARTESIAN_POINT('Ctrl Pts',(108.518334029221,11.5234918702337,8.51867896338995));
#103371=CARTESIAN_POINT('Ctrl Pts',(108.443678257074,10.8824597405917,8.56466729034773));
#103372=CARTESIAN_POINT('Ctrl Pts',(108.444807264591,10.7513287041109,8.5740562256037));
#103373=CARTESIAN_POINT('Origin',(110.,10.75,5.2859437743963));
#103374=CARTESIAN_POINT('',(108.443317976897,10.7511999786121,7.0359437743963));
#103375=CARTESIAN_POINT('',(108.446877037961,10.7499579969204,7.17405622560371));
#103376=CARTESIAN_POINT('',(108.4445,10.7499999999999,5.2859437743963));
#103377=CARTESIAN_POINT('Ctrl Pts',(108.443317976897,10.7511999786121,7.0359437743963));
#103378=CARTESIAN_POINT('Ctrl Pts',(108.446869824562,10.3191164320538,7.06695947477319));
#103379=CARTESIAN_POINT('Ctrl Pts',(108.856701971244,9.37104702086914,7.13457456685187));
#103380=CARTESIAN_POINT('Ctrl Pts',(110.452949548444,8.97578890357189,7.23878905063235));
#103381=CARTESIAN_POINT('Ctrl Pts',(111.729171099463,10.1474049425682,7.34858722573775));
#103382=CARTESIAN_POINT('Ctrl Pts',(111.457504537093,11.8585497627777,7.45838540084314));
#103383=CARTESIAN_POINT('Ctrl Pts',(109.881084321976,12.5772916662981,7.56818357594853));
#103384=CARTESIAN_POINT('Ctrl Pts',(108.642449345411,11.8046002560737,7.66070303379958));
#103385=CARTESIAN_POINT('Ctrl Pts',(108.447198281137,11.0205182619924,7.71662309994884));
#103386=CARTESIAN_POINT('Ctrl Pts',(108.446844740062,10.7497785244693,7.7359437743963));
#103387=CARTESIAN_POINT('Ctrl Pts',(108.446877037961,10.7499579969204,7.17405622560371));
#103388=CARTESIAN_POINT('Ctrl Pts',(108.446805685801,10.4965188357708,7.19214125659283));
#103389=CARTESIAN_POINT('Ctrl Pts',(108.624301182411,9.73027362155383,7.24682567928375));
#103390=CARTESIAN_POINT('Ctrl Pts',(109.82036714101,8.92767494081165,7.33810949367647));
#103391=CARTESIAN_POINT('Ctrl Pts',(111.41981313278,9.59358681487167,7.44790766878186));
#103392=CARTESIAN_POINT('Ctrl Pts',(111.748271359623,11.29471174246,7.55770584388725));
#103393=CARTESIAN_POINT('Ctrl Pts',(110.511701824797,12.5082142882526,7.66750401899264));
#103394=CARTESIAN_POINT('Ctrl Pts',(108.884174677395,12.1620667174056,7.77295414623146));
#103395=CARTESIAN_POINT('Ctrl Pts',(108.446109530629,11.1980291091366,7.84180488176848));
#103396=CARTESIAN_POINT('Ctrl Pts',(108.442854064965,10.7490502583051,7.8740562256037));
#103397=CARTESIAN_POINT('Origin',(110.,10.75,13.926));
#103398=CARTESIAN_POINT('',(109.07607384819,9.02823449157528,13.926));
#103399=CARTESIAN_POINT('Ctrl Pts',(109.140566776777,12.049156215532,13.926));
#103400=CARTESIAN_POINT('Ctrl Pts',(109.096212441881,12.0275126749281,13.926));
#103401=CARTESIAN_POINT('Ctrl Pts',(109.053058974181,12.0037020680889,13.926));
#103402=CARTESIAN_POINT('Ctrl Pts',(109.011284708367,11.9777581097249,13.926));
#103403=CARTESIAN_POINT('Ctrl Pts',(108.960679148907,11.9463294657494,13.926));
#103404=CARTESIAN_POINT('Ctrl Pts',(108.912096233717,11.9117718230936,13.926));
#103405=CARTESIAN_POINT('Ctrl Pts',(108.86562338902,11.8743978959904,13.926));
#103406=CARTESIAN_POINT('Ctrl Pts',(108.850452021899,11.8621969306191,13.926));
#103407=CARTESIAN_POINT('Ctrl Pts',(108.835505668127,11.8496954296351,13.926));
#103408=CARTESIAN_POINT('Ctrl Pts',(108.820787810844,11.8369031865342,13.926));
#103409=CARTESIAN_POINT('Ctrl Pts',(108.80591914035,11.8239798619021,13.926));
#103410=CARTESIAN_POINT('Ctrl Pts',(108.791278940907,11.810755083877,13.926));
#103411=CARTESIAN_POINT('Ctrl Pts',(108.77689730581,11.797263909003,13.926));
#103412=CARTESIAN_POINT('Ctrl Pts',(108.731524838567,11.7547007452223,13.926));
#103413=CARTESIAN_POINT('Ctrl Pts',(108.688682887307,11.7094570944331,13.926));
#103414=CARTESIAN_POINT('Ctrl Pts',(108.648464424372,11.6618791784732,13.926));
#103415=CARTESIAN_POINT('Ctrl Pts',(108.616938129699,11.6245839839531,13.926));
#103416=CARTESIAN_POINT('Ctrl Pts',(108.58702407997,11.5858532354006,13.926));
#103417=CARTESIAN_POINT('Ctrl Pts',(108.558777269814,11.5458338354115,13.926));
#103418=CARTESIAN_POINT('Ctrl Pts',(108.546234964393,11.5280641993131,13.926));
#103419=CARTESIAN_POINT('Ctrl Pts',(108.53402150688,11.5100402877822,13.926));
#103420=CARTESIAN_POINT('Ctrl Pts',(108.522142432535,11.4917740517978,13.926));
#103421=CARTESIAN_POINT('Ctrl Pts',(108.515052248395,11.4808716049466,13.926));
#103422=CARTESIAN_POINT('Ctrl Pts',(108.508085351031,11.469889115632,13.926));
#103423=CARTESIAN_POINT('Ctrl Pts',(108.501246091907,11.4588352992566,13.926));
#103424=CARTESIAN_POINT('Ctrl Pts',(108.46722064447,11.4038423473526,13.926));
#103425=CARTESIAN_POINT('Ctrl Pts',(108.436323746455,11.3470439400103,13.926));
#103426=CARTESIAN_POINT('Ctrl Pts',(108.408653404881,11.2887905666606,13.926));
#103427=CARTESIAN_POINT('Ctrl Pts',(108.380421099685,11.2293541115438,13.926));
#103428=CARTESIAN_POINT('Ctrl Pts',(108.355546974404,11.1684022291955,13.926));
#103429=CARTESIAN_POINT('Ctrl Pts',(108.334168214284,11.1062649443926,13.926));
#103430=CARTESIAN_POINT('Ctrl Pts',(108.319757574467,11.0643804746918,13.926));
#103431=CARTESIAN_POINT('Ctrl Pts',(108.306935789132,11.0219565288301,13.926));
#103432=CARTESIAN_POINT('Ctrl Pts',(108.295755797419,10.9790864894013,13.926));
#103433=CARTESIAN_POINT('Ctrl Pts',(108.28804833841,10.9495319888175,13.926));
#103434=CARTESIAN_POINT('Ctrl Pts',(108.281121359323,10.919765349962,13.926));
#103435=CARTESIAN_POINT('Ctrl Pts',(108.274995069302,10.8898160442948,13.926));
#103436=CARTESIAN_POINT('Ctrl Pts',(108.273006324846,10.8800937628803,13.926));
#103437=CARTESIAN_POINT('Ctrl Pts',(108.27110240947,10.8703540703402,13.926));
#103438=CARTESIAN_POINT('Ctrl Pts',(108.269285497152,10.8606070238497,13.926));
#103439=CARTESIAN_POINT('Ctrl Pts',(108.256865790514,10.7939800012846,13.926));
#103440=CARTESIAN_POINT('Ctrl Pts',(108.248483734475,10.7268949524802,13.926));
#103441=CARTESIAN_POINT('Ctrl Pts',(108.244266995922,10.659703975981,13.926));
#103442=CARTESIAN_POINT('Ctrl Pts',(108.242731581514,10.6352381495744,13.926));
#103443=CARTESIAN_POINT('Ctrl Pts',(108.241748823705,10.6107579684671,13.926));
#103444=CARTESIAN_POINT('Ctrl Pts',(108.24132633562,10.5862795120633,13.926));
#103445=CARTESIAN_POINT('Ctrl Pts',(108.240204685504,10.521292440333,13.926));
#103446=CARTESIAN_POINT('Ctrl Pts',(108.243028159913,10.4563182246449,13.926));
#103447=CARTESIAN_POINT('Ctrl Pts',(108.249591140909,10.391599767868,13.926));
#103448=CARTESIAN_POINT('Ctrl Pts',(108.253023120763,10.3577565432754,13.926));
#103449=CARTESIAN_POINT('Ctrl Pts',(108.257478553759,10.3239830677188,13.926));
#103450=CARTESIAN_POINT('Ctrl Pts',(108.26293352207,10.2903134507712,13.926));
#103451=CARTESIAN_POINT('Ctrl Pts',(108.265675912799,10.273386634687,13.926));
#103452=CARTESIAN_POINT('Ctrl Pts',(108.268670983993,10.2564860659407,13.926));
#103453=CARTESIAN_POINT('Ctrl Pts',(108.271916040856,10.2396160874463,13.926));
#103454=CARTESIAN_POINT('Ctrl Pts',(108.274212856499,10.2276757017639,13.926));
#103455=CARTESIAN_POINT('Ctrl Pts',(108.276635216349,10.2157492185281,13.926));
#103456=CARTESIAN_POINT('Ctrl Pts',(108.279181283577,10.2038426088341,13.926));
#103457=CARTESIAN_POINT('Ctrl Pts',(108.293323163217,10.1377085180316,13.926));
#103458=CARTESIAN_POINT('Ctrl Pts',(108.311217290379,10.0724644861745,13.926));
#103459=CARTESIAN_POINT('Ctrl Pts',(108.332610647139,10.0083733770064,13.926));
#103460=CARTESIAN_POINT('Ctrl Pts',(108.354477710045,9.94286311923765,13.926));
#103461=CARTESIAN_POINT('Ctrl Pts',(108.380000809587,9.87855654185356,13.926));
#103462=CARTESIAN_POINT('Ctrl Pts',(108.408964920281,9.81572791433377,13.926));
#103463=CARTESIAN_POINT('Ctrl Pts',(108.438204666487,9.75230138131932,13.926));
#103464=CARTESIAN_POINT('Ctrl Pts',(108.470951499624,9.69038007622194,13.926));
#103465=CARTESIAN_POINT('Ctrl Pts',(108.507036609764,9.63025378709743,13.926));
#103466=CARTESIAN_POINT('Ctrl Pts',(108.521435797672,9.60626134999678,13.926));
#103467=CARTESIAN_POINT('Ctrl Pts',(108.53636709129,9.58255489670699,13.926));
#103468=CARTESIAN_POINT('Ctrl Pts',(108.551821908304,9.55915372538839,13.926));
#103469=CARTESIAN_POINT('Ctrl Pts',(108.55754106392,9.55049396964837,13.926));
#103470=CARTESIAN_POINT('Ctrl Pts',(108.563330918209,9.54187763709662,13.926));
#103471=CARTESIAN_POINT('Ctrl Pts',(108.569185682118,9.53331319880462,13.926));
#103472=CARTESIAN_POINT('Ctrl Pts',(108.60991484744,9.47373395213159,13.926));
#103473=CARTESIAN_POINT('Ctrl Pts',(108.653849190263,9.41656157277207,13.926));
#103474=CARTESIAN_POINT('Ctrl Pts',(108.700756166978,9.36208419964962,13.926));
#103475=CARTESIAN_POINT('Ctrl Pts',(108.747781963714,9.30746882994174,13.926));
#103476=CARTESIAN_POINT('Ctrl Pts',(108.797795870477,9.2555611149366,13.926));
#103477=CARTESIAN_POINT('Ctrl Pts',(108.850613754612,9.20666582811862,13.926));
#103478=CARTESIAN_POINT('Ctrl Pts',(108.902318938299,9.15880060542464,13.926));
#103479=CARTESIAN_POINT('Ctrl Pts',(108.956711742704,9.11382134718746,13.926));
#103480=CARTESIAN_POINT('Ctrl Pts',(109.013660238129,9.0720416880423,13.926));
#103481=CARTESIAN_POINT('Ctrl Pts',(109.034135713973,9.05702007254222,13.926));
#103482=CARTESIAN_POINT('Ctrl Pts',(109.054941918824,9.04241240218612,13.926));
#103483=CARTESIAN_POINT('Ctrl Pts',(109.07607384819,9.02823449157529,13.926));
#103484=CARTESIAN_POINT('',(108.046,10.75,13.926));
#103485=CARTESIAN_POINT('Origin',(110.,10.75,13.926));
#103486=CARTESIAN_POINT('',(110.799022681602,8.96531988605745,13.926));
#103487=CARTESIAN_POINT('Origin',(110.,10.75,13.926));
#103488=CARTESIAN_POINT('Ctrl Pts',(110.800030261768,8.96425629420691,13.926));
#103489=CARTESIAN_POINT('Ctrl Pts',(110.853254520143,8.99427974873486,13.926));
#103490=CARTESIAN_POINT('Ctrl Pts',(110.904869181937,9.02687709790755,13.926));
#103491=CARTESIAN_POINT('Ctrl Pts',(110.954657890784,9.06206156501285,13.926));
#103492=CARTESIAN_POINT('Ctrl Pts',(111.013441596184,9.10360257695933,13.926));
#103493=CARTESIAN_POINT('Ctrl Pts',(111.069681245781,9.14875005427251,13.926));
#103494=CARTESIAN_POINT('Ctrl Pts',(111.123200852482,9.19717009084562,13.926));
#103495=CARTESIAN_POINT('Ctrl Pts',(111.146304270927,9.21807211974725,13.926));
#103496=CARTESIAN_POINT('Ctrl Pts',(111.168900259238,9.23958434779001,13.926));
#103497=CARTESIAN_POINT('Ctrl Pts',(111.190972005754,9.26168122696303,13.926));
#103498=CARTESIAN_POINT('Ctrl Pts',(111.201661060319,9.27238245294035,13.926));
#103499=CARTESIAN_POINT('Ctrl Pts',(111.212227772727,9.28322163766534,13.926));
#103500=CARTESIAN_POINT('Ctrl Pts',(111.222658638307,9.2941834023316,13.926));
#103501=CARTESIAN_POINT('Ctrl Pts',(111.271809717873,9.34583612119508,13.926));
#103502=CARTESIAN_POINT('Ctrl Pts',(111.318010893287,9.40026995040382,13.926));
#103503=CARTESIAN_POINT('Ctrl Pts',(111.361098000433,9.45715214147117,13.926));
#103504=CARTESIAN_POINT('Ctrl Pts',(111.392784241534,9.49898328168631,13.926));
#103505=CARTESIAN_POINT('Ctrl Pts',(111.422785486411,9.54213928816585,13.926));
#103506=CARTESIAN_POINT('Ctrl Pts',(111.451019604943,9.58649413012682,13.926));
#103507=CARTESIAN_POINT('Ctrl Pts',(111.465995132324,9.61002017537955,13.926));
#103508=CARTESIAN_POINT('Ctrl Pts',(111.480473263727,9.63388355125054,13.926));
#103509=CARTESIAN_POINT('Ctrl Pts',(111.494439972729,9.65806567929226,13.926));
#103510=CARTESIAN_POINT('Ctrl Pts',(111.500869702427,9.66919819066671,13.926));
#103511=CARTESIAN_POINT('Ctrl Pts',(111.507191762579,9.6803997476648,13.926));
#103512=CARTESIAN_POINT('Ctrl Pts',(111.51339693583,9.69165399486125,13.926));
#103513=CARTESIAN_POINT('Ctrl Pts',(111.547016349844,9.75262911684645,13.926));
#103514=CARTESIAN_POINT('Ctrl Pts',(111.577261792345,9.81523933357153,13.926));
#103515=CARTESIAN_POINT('Ctrl Pts',(111.603978750335,9.87917776379081,13.926));
#103516=CARTESIAN_POINT('Ctrl Pts',(111.630092665242,9.94167300470077,13.926));
#103517=CARTESIAN_POINT('Ctrl Pts',(111.65283571523,10.005438163468,13.926));
#103518=CARTESIAN_POINT('Ctrl Pts',(111.672015533369,10.0701944516723,13.926));
#103519=CARTESIAN_POINT('Ctrl Pts',(111.685399646162,10.11538286061,13.926));
#103520=CARTESIAN_POINT('Ctrl Pts',(111.697047632966,10.161054073457,13.926));
#103521=CARTESIAN_POINT('Ctrl Pts',(111.706879216135,10.2071119606939,13.926));
#103522=CARTESIAN_POINT('Ctrl Pts',(111.71515302186,10.2458721486039,13.926));
#103523=CARTESIAN_POINT('Ctrl Pts',(111.722140229568,10.2849062042654,13.926));
#103524=CARTESIAN_POINT('Ctrl Pts',(111.727785830159,10.324154890653,13.926));
#103525=CARTESIAN_POINT('Ctrl Pts',(111.729386111696,10.3352801814318,13.926));
#103526=CARTESIAN_POINT('Ctrl Pts',(111.73087832549,10.3464216841658,13.926));
#103527=CARTESIAN_POINT('Ctrl Pts',(111.732259848983,10.3575652207405,13.926));
#103528=CARTESIAN_POINT('Ctrl Pts',(111.740282047033,10.4222732462359,13.926));
#103529=CARTESIAN_POINT('Ctrl Pts',(111.744593192869,10.4871654619733,13.926));
#103530=CARTESIAN_POINT('Ctrl Pts',(111.745022935266,10.5519847273788,13.926));
#103531=CARTESIAN_POINT('Ctrl Pts',(111.745188833282,10.5770075958328,13.926));
#103532=CARTESIAN_POINT('Ctrl Pts',(111.744775756678,10.6020195479022,13.926));
#103533=CARTESIAN_POINT('Ctrl Pts',(111.743771826316,10.6270054623453,13.926));
#103534=CARTESIAN_POINT('Ctrl Pts',(111.741048994449,10.6947715611111,13.926));
#103535=CARTESIAN_POINT('Ctrl Pts',(111.733983491,10.7623480550873,13.926));
#103536=CARTESIAN_POINT('Ctrl Pts',(111.722746501004,10.8294016522599,13.926));
#103537=CARTESIAN_POINT('Ctrl Pts',(111.717656379603,10.8597755290813,13.926));
#103538=CARTESIAN_POINT('Ctrl Pts',(111.711709616642,10.8900417576836,13.926));
#103539=CARTESIAN_POINT('Ctrl Pts',(111.704918977153,10.9201671810666,13.926));
#103540=CARTESIAN_POINT('Ctrl Pts',(111.700644111634,10.9391318358552,13.926));
#103541=CARTESIAN_POINT('Ctrl Pts',(111.696034781489,10.9580406592758,13.926));
#103542=CARTESIAN_POINT('Ctrl Pts',(111.691093828577,10.9768850263927,13.926));
#103543=CARTESIAN_POINT('Ctrl Pts',(111.687299350237,10.9913568386387,13.926));
#103544=CARTESIAN_POINT('Ctrl Pts',(111.683307875461,11.0057949971679,13.926));
#103545=CARTESIAN_POINT('Ctrl Pts',(111.679129091647,11.0201676983228,13.926));
#103546=CARTESIAN_POINT('Ctrl Pts',(111.661041641071,11.0823785073483,13.926));
#103547=CARTESIAN_POINT('Ctrl Pts',(111.639426529773,11.1434585617679,13.926));
#103548=CARTESIAN_POINT('Ctrl Pts',(111.614463340613,11.2031288954202,13.926));
#103549=CARTESIAN_POINT('Ctrl Pts',(111.589577411983,11.2626145506798,13.926));
#103550=CARTESIAN_POINT('Ctrl Pts',(111.561363371937,11.320700065467,13.926));
#103551=CARTESIAN_POINT('Ctrl Pts',(111.529957992456,11.3770783554949,13.926));
#103552=CARTESIAN_POINT('Ctrl Pts',(111.499178456137,11.4323331447748,13.926));
#103553=CARTESIAN_POINT('Ctrl Pts',(111.465332776718,11.4859487286863,13.926));
#103554=CARTESIAN_POINT('Ctrl Pts',(111.428521000927,11.5375954324615,13.926));
#103555=CARTESIAN_POINT('Ctrl Pts',(111.420177735821,11.5493009840742,13.926));
#103556=CARTESIAN_POINT('Ctrl Pts',(111.41168201237,11.5609052067453,13.926));
#103557=CARTESIAN_POINT('Ctrl Pts',(111.403034843024,11.5724039121731,13.926));
#103558=CARTESIAN_POINT('Ctrl Pts',(111.396582580946,11.5809839061578,13.926));
#103559=CARTESIAN_POINT('Ctrl Pts',(111.390051334627,11.5894980275904,13.926));
#103560=CARTESIAN_POINT('Ctrl Pts',(111.383443257475,11.5979431486214,13.926));
#103561=CARTESIAN_POINT('Ctrl Pts',(111.345215317679,11.6467984466027,13.926));
#103562=CARTESIAN_POINT('Ctrl Pts',(111.304403622696,11.6933678052254,13.926));
#103563=CARTESIAN_POINT('Ctrl Pts',(111.261138232155,11.7373789713312,13.926));
#103564=CARTESIAN_POINT('Ctrl Pts',(111.218651929526,11.7805976202061,13.926));
#103565=CARTESIAN_POINT('Ctrl Pts',(111.173798814374,11.8213499371724,13.926));
#103566=CARTESIAN_POINT('Ctrl Pts',(111.126677325675,11.8593349320108,13.926));
#103567=CARTESIAN_POINT('Ctrl Pts',(111.081054798031,11.8961116028012,13.926));
#103568=CARTESIAN_POINT('Ctrl Pts',(111.033305320964,11.9302945290462,13.926));
#103569=CARTESIAN_POINT('Ctrl Pts',(110.983504216739,11.961563551928,13.926));
#103570=CARTESIAN_POINT('Ctrl Pts',(110.971937739318,11.9688258898376,13.926));
#103571=CARTESIAN_POINT('Ctrl Pts',(110.960260553415,11.9759308302077,13.926));
#103572=CARTESIAN_POINT('Ctrl Pts',(110.948473540785,11.982873956425,13.926));
#103573=CARTESIAN_POINT('Ctrl Pts',(109.314174270871,12.1461458803668,6.34992591772793));
#103574=CARTESIAN_POINT('Ctrl Pts',(108.85551888803,11.9208415860382,6.38652530942973));
#103575=CARTESIAN_POINT('Ctrl Pts',(108.18502735973,10.9866824883096,6.45972409283332));
#103576=CARTESIAN_POINT('Ctrl Pts',(108.80047449685,9.36512639286223,6.56952226793872));
#103577=CARTESIAN_POINT('Ctrl Pts',(110.491593333654,8.98640096532305,6.67932044304411));
#103578=CARTESIAN_POINT('Ctrl Pts',(111.741732863822,10.1849114394086,6.7891186181495));
#103579=CARTESIAN_POINT('Ctrl Pts',(111.433149639798,11.8900189191182,6.8989167932549));
#103580=CARTESIAN_POINT('Ctrl Pts',(109.841413191019,12.5742367163702,7.00871496836029));
#103581=CARTESIAN_POINT('Ctrl Pts',(108.391749493731,11.6256052224506,7.11851314346568));
#103582=CARTESIAN_POINT('Ctrl Pts',(108.38171275925,9.89305824642555,7.22831131857108));
#103583=CARTESIAN_POINT('Ctrl Pts',(109.82036714101,8.92767494081165,7.33810949367647));
#103584=CARTESIAN_POINT('Ctrl Pts',(111.41981313278,9.59358681487167,7.44790766878186));
#103585=CARTESIAN_POINT('Ctrl Pts',(111.748271359623,11.29471174246,7.55770584388725));
#103586=CARTESIAN_POINT('Ctrl Pts',(110.511701824797,12.5082142882526,7.66750401899264));
#103587=CARTESIAN_POINT('Ctrl Pts',(108.817066499089,12.1477939398722,7.77730219409804));
#103588=CARTESIAN_POINT('Ctrl Pts',(108.181373638266,10.5360895014301,7.88710036920342));
#103589=CARTESIAN_POINT('Ctrl Pts',(109.173686477906,9.11587493853038,7.99689854430882));
#103590=CARTESIAN_POINT('Ctrl Pts',(110.90570183064,9.15850278599423,8.10669671941421));
#103591=CARTESIAN_POINT('Ctrl Pts',(111.8269474297,10.6258137189513,8.2164948945196));
#103592=CARTESIAN_POINT('Ctrl Pts',(111.112738765821,12.2042941592694,8.32629306962499));
#103593=CARTESIAN_POINT('Ctrl Pts',(109.402424116335,12.4809136837355,8.43609124473039));
#103594=CARTESIAN_POINT('Ctrl Pts',(108.227049862518,11.2080468503276,8.54588941983577));
#103595=CARTESIAN_POINT('Ctrl Pts',(108.638792317746,9.52514378590672,8.65568759494117));
#103596=CARTESIAN_POINT('Ctrl Pts',(110.269066191156,8.93871247704089,8.76548577004656));
#103597=CARTESIAN_POINT('Ctrl Pts',(111.658476300169,9.97371689050704,8.87528394515196));
#103598=CARTESIAN_POINT('Ctrl Pts',(111.563244859267,11.7036375693259,8.98508212025735));
#103599=CARTESIAN_POINT('Ctrl Pts',(110.068621537362,12.5798770967034,9.09488029536274));
#103600=CARTESIAN_POINT('Ctrl Pts',(108.512569308827,11.8180398134534,9.20467847046814));
#103601=CARTESIAN_POINT('Ctrl Pts',(108.288041326803,10.1001103129093,9.31447664557353));
#103602=CARTESIAN_POINT('Ctrl Pts',(109.596031461916,8.9639517015356,9.42427482067892));
#103603=CARTESIAN_POINT('Ctrl Pts',(111.265647793446,9.42663505898133,9.53407299578432));
#103604=CARTESIAN_POINT('Ctrl Pts',(111.802276393556,11.073973618372,9.6438711708897));
#103605=CARTESIAN_POINT('Ctrl Pts',(110.725535892815,12.4312961584497,9.7536693459951));
#103606=CARTESIAN_POINT('Ctrl Pts',(108.99930722521,12.2835491758203,9.86346752110049));
#103607=CARTESIAN_POINT('Ctrl Pts',(108.16888277946,10.7629934143855,9.97326569620588));
#103608=CARTESIAN_POINT('Ctrl Pts',(108.977645283184,9.23080615549536,10.0830638713113));
#103609=CARTESIAN_POINT('Ctrl Pts',(110.701603433992,9.05857701162966,10.1928620464167));
#103610=CARTESIAN_POINT('Ctrl Pts',(111.797497373615,10.4004827672002,10.3026602215221));
#103611=CARTESIAN_POINT('Ctrl Pts',(111.284300314861,12.0552707785837,10.4124583966274));
#103612=CARTESIAN_POINT('Ctrl Pts',(109.621418084829,12.5416011938169,10.5222565717329));
#103613=CARTESIAN_POINT('Ctrl Pts',(108.297436351006,11.4241187768446,10.6320547468382));
#103614=CARTESIAN_POINT('Ctrl Pts',(108.497562458434,9.70317597569252,10.7418529219436));
#103615=CARTESIAN_POINT('Ctrl Pts',(110.042646705583,8.91933335565637,10.851651097049));
#103616=CARTESIAN_POINT('Ctrl Pts',(111.549554301631,9.77427433649753,10.9614492721544));
#103617=CARTESIAN_POINT('Ctrl Pts',(111.669325585378,11.5026693790562,11.0712474472598));
#103618=CARTESIAN_POINT('Ctrl Pts',(110.294743212587,12.5572867904855,11.1810456223652));
#103619=CARTESIAN_POINT('Ctrl Pts',(108.656311413926,11.99404987332,11.2908437974706));
#103620=CARTESIAN_POINT('Ctrl Pts',(108.220728220139,10.3171593391372,11.400641972576));
#103621=CARTESIAN_POINT('Ctrl Pts',(109.377920764104,9.02774086435358,11.5104401476814));
#103622=CARTESIAN_POINT('Ctrl Pts',(111.091988723841,9.28006131881894,11.6202383227868));
#103623=CARTESIAN_POINT('Ctrl Pts',(111.82852578498,10.8482474465615,11.7300364978922));
#103624=CARTESIAN_POINT('Ctrl Pts',(110.928195705052,12.3284840355239,11.8398346729976));
#103625=CARTESIAN_POINT('Ctrl Pts',(109.196959631481,12.3956868563535,11.9496328481029));
#103626=CARTESIAN_POINT('Ctrl Pts',(108.184592481991,10.989697073083,12.0594310232083));
#103627=CARTESIAN_POINT('Ctrl Pts',(108.797349235318,9.36913421129256,12.1692291983137));
#103628=CARTESIAN_POINT('Ctrl Pts',(110.486699725726,8.98470055506267,12.2790273734191));
#103629=CARTESIAN_POINT('Ctrl Pts',(111.74036449784,10.1805344965231,12.3888255485245));
#103630=CARTESIAN_POINT('Ctrl Pts',(111.436082469949,11.8861455476417,12.4986237236299));
#103631=CARTESIAN_POINT('Ctrl Pts',(109.846242795973,12.5746958549649,12.6084218987353));
#103632=CARTESIAN_POINT('Ctrl Pts',(108.394043120869,11.6298102816096,12.7182200738407));
#103633=CARTESIAN_POINT('Ctrl Pts',(108.379472480118,9.897326941871,12.8280182489461));
#103634=CARTESIAN_POINT('Ctrl Pts',(109.815568107276,8.92815438021742,12.9378164240515));
#103635=CARTESIAN_POINT('Ctrl Pts',(111.416772645554,9.58984568552079,13.0476145991569));
#103636=CARTESIAN_POINT('Ctrl Pts',(111.749687759447,11.2901360392881,13.1574127742623));
#103637=CARTESIAN_POINT('Ctrl Pts',(110.516345144641,12.5068087730147,13.2672109493676));
#103638=CARTESIAN_POINT('Ctrl Pts',(108.820707641908,12.1510105496194,13.377009124473));
#103639=CARTESIAN_POINT('Ctrl Pts',(108.180898216782,10.5406506448061,13.4868072995784));
#103640=CARTESIAN_POINT('Ctrl Pts',(109.169225983483,9.11850985467691,13.5966054746838));
#103641=CARTESIAN_POINT('Ctrl Pts',(110.901845461742,9.15519245562723,13.7064036497892));
#103642=CARTESIAN_POINT('Ctrl Pts',(111.825924765157,10.6229447474917,13.8162018248946));
#103643=CARTESIAN_POINT('Ctrl Pts',(111.353491586843,11.6712858186231,13.8894006082982));
#103644=CARTESIAN_POINT('Ctrl Pts',(110.948473540785,11.982873956425,13.926));
#103645=CARTESIAN_POINT('Ctrl Pts',(109.255607560691,12.2653710241204,6.42661727848529));
#103646=CARTESIAN_POINT('Ctrl Pts',(108.757784885433,12.0208266652274,6.46321667018709));
#103647=CARTESIAN_POINT('Ctrl Pts',(108.030036124939,11.006894204069,6.53641545359068));
#103648=CARTESIAN_POINT('Ctrl Pts',(108.698039928543,9.24686385510494,6.64621362869608));
#103649=CARTESIAN_POINT('Ctrl Pts',(110.533573392254,8.83579682617836,6.75601180380147));
#103650=CARTESIAN_POINT('Ctrl Pts',(111.890469721474,10.1366551892434,6.86580997890685));
#103651=CARTESIAN_POINT('Ctrl Pts',(111.55553475315,11.9873718687096,6.97560815401225));
#103652=CARTESIAN_POINT('Ctrl Pts',(109.827870526628,12.7300190653413,7.08540632911764));
#103653=CARTESIAN_POINT('Ctrl Pts',(108.254411483071,11.7003783245928,7.19520450422304));
#103654=CARTESIAN_POINT('Ctrl Pts',(108.243517652545,9.81987892813574,7.30500267932843));
#103655=CARTESIAN_POINT('Ctrl Pts',(109.80502723009,8.77205583953947,7.41480085443382));
#103656=CARTESIAN_POINT('Ctrl Pts',(111.54105936302,9.49483386206473,7.52459902953921));
#103657=CARTESIAN_POINT('Ctrl Pts',(111.897566578055,11.3412278957591,7.6343972046446));
#103658=CARTESIAN_POINT('Ctrl Pts',(110.555399066238,12.6583585920924,7.74419537975));
#103659=CARTESIAN_POINT('Ctrl Pts',(108.716048819862,12.2671598211621,7.85399355485539));
#103660=CARTESIAN_POINT('Ctrl Pts',(108.026070390618,10.5178224203886,7.96379172996078));
#103661=CARTESIAN_POINT('Ctrl Pts',(109.103122685223,8.97632734676019,8.07358990506617));
#103662=CARTESIAN_POINT('Ctrl Pts',(110.983045059936,9.02259543792151,8.18338808017156));
#103663=CARTESIAN_POINT('Ctrl Pts',(111.982961262494,10.6152087188446,8.29318625527695));
#103664=CARTESIAN_POINT('Ctrl Pts',(111.207762101979,12.3284849280402,8.40298443038235));
#103665=CARTESIAN_POINT('Ctrl Pts',(109.35139358175,12.6287266276911,8.51278260548774));
#103666=CARTESIAN_POINT('Ctrl Pts',(108.075647177468,11.2471621765583,8.62258078059314));
#103667=CARTESIAN_POINT('Ctrl Pts',(108.522550753109,9.42054607856372,8.73237895569852));
#103668=CARTESIAN_POINT('Ctrl Pts',(110.292043342592,8.78403593618604,8.84217713080392));
#103669=CARTESIAN_POINT('Ctrl Pts',(111.800103388054,9.90742549028566,8.95197530590931));
#103670=CARTESIAN_POINT('Ctrl Pts',(111.696739571882,11.7850743145046,9.0617734810147));
#103671=CARTESIAN_POINT('Ctrl Pts',(110.074481535784,12.7361411110688,9.1715716561201));
#103672=CARTESIAN_POINT('Ctrl Pts',(108.385548815859,11.9092460420318,9.28136983122549));
#103673=CARTESIAN_POINT('Ctrl Pts',(108.141847063164,10.0446123936324,9.39116800633088));
#103674=CARTESIAN_POINT('Ctrl Pts',(109.561534202208,8.81143048714838,9.50096618143628));
#103675=CARTESIAN_POINT('Ctrl Pts',(111.373728934706,9.31362510955542,9.61076435654167));
#103676=CARTESIAN_POINT('Ctrl Pts',(111.956183420843,11.1016396393559,9.72056253164705));
#103677=CARTESIAN_POINT('Ctrl Pts',(110.787493688441,12.5748719688305,9.83036070675245));
#103678=CARTESIAN_POINT('Ctrl Pts',(108.913852158082,12.4145079986135,9.94015888185784));
#103679=CARTESIAN_POINT('Ctrl Pts',(108.012512863595,10.764102998792,10.0499570569632));
#103680=CARTESIAN_POINT('Ctrl Pts',(108.890340374869,9.10107321924012,10.1597552320686));
#103681=CARTESIAN_POINT('Ctrl Pts',(110.76151749559,8.91413641142274,10.269553407174));
#103682=CARTESIAN_POINT('Ctrl Pts',(111.950996292159,10.3706354260943,10.3793515822794));
#103683=CARTESIAN_POINT('Ctrl Pts',(111.393974305104,12.1667355605971,10.4891497573848));
#103684=CARTESIAN_POINT('Ctrl Pts',(109.58908873881,12.6945966027392,10.5989479324902));
#103685=CARTESIAN_POINT('Ctrl Pts',(108.15204438398,11.4816857612167,10.7087461075956));
#103686=CARTESIAN_POINT('Ctrl Pts',(108.369260441867,9.61378148867087,10.818544282701));
#103687=CARTESIAN_POINT('Ctrl Pts',(110.046288559686,8.76300191715408,10.9283424578064));
#103688=CARTESIAN_POINT('Ctrl Pts',(111.68187989666,9.69095135848281,11.0381406329118));
#103689=CARTESIAN_POINT('Ctrl Pts',(111.811879157814,11.5669442633493,11.1479388080172));
#103690=CARTESIAN_POINT('Ctrl Pts',(110.319913076557,12.7116216851622,11.2577369831225));
#103691=CARTESIAN_POINT('Ctrl Pts',(108.541565908397,12.1002866406013,11.3675351582279));
#103692=CARTESIAN_POINT('Ctrl Pts',(108.068785692704,10.2801965183178,11.4773333333333));
#103693=CARTESIAN_POINT('Ctrl Pts',(109.324797743531,8.88066698338174,11.5871315084387));
#103694=CARTESIAN_POINT('Ctrl Pts',(111.185240091344,9.15453457190998,11.6969296835441));
#103695=CARTESIAN_POINT('Ctrl Pts',(111.984674402855,10.8566373763707,11.8067278586495));
#103696=CARTESIAN_POINT('Ctrl Pts',(111.007459819155,12.4632801114172,11.9165260337549));
#103697=CARTESIAN_POINT('Ctrl Pts',(109.128383270856,12.5362217780843,12.0263242088603));
#103698=CARTESIAN_POINT('Ctrl Pts',(108.029564110423,11.0101662220434,12.1361223839657));
#103699=CARTESIAN_POINT('Ctrl Pts',(108.694647782467,9.2512139248252,12.2459205590711));
#103700=CARTESIAN_POINT('Ctrl Pts',(110.52826189024,8.83395120784152,12.3557187341765));
#103701=CARTESIAN_POINT('Ctrl Pts',(111.888984502638,10.1319044733503,12.4655169092819));
#103702=CARTESIAN_POINT('Ctrl Pts',(111.558718034992,11.9831677271628,12.5753150843873));
#103703=CARTESIAN_POINT('Ctrl Pts',(109.833112560077,12.7305174124926,12.6851132594926));
#103704=CARTESIAN_POINT('Ctrl Pts',(108.256900976578,11.7049424785926,12.7949114345981));
#103705=CARTESIAN_POINT('Ctrl Pts',(108.241086062745,9.82451215270046,12.9047096097034));
#103706=CARTESIAN_POINT('Ctrl Pts',(109.799818378518,8.77257622110816,13.0145077848088));
#103707=CARTESIAN_POINT('Ctrl Pts',(111.537759230629,9.49077325557974,13.1243059599142));
#103708=CARTESIAN_POINT('Ctrl Pts',(111.899103932626,11.3362614462647,13.2341041350196));
#103709=CARTESIAN_POINT('Ctrl Pts',(110.560438906591,12.656833051606,13.343902310125));
#103710=CARTESIAN_POINT('Ctrl Pts',(108.720000901374,12.2706511162161,13.4537004852304));
#103711=CARTESIAN_POINT('Ctrl Pts',(108.025554370084,10.5227730667402,13.5634986603358));
#103712=CARTESIAN_POINT('Ctrl Pts',(109.098281282833,8.9791872739609,13.6732968354412));
#103713=CARTESIAN_POINT('Ctrl Pts',(110.978859372918,9.01900241889038,13.7830950105466));
#103714=CARTESIAN_POINT('Ctrl Pts',(111.981851266585,10.612094748965,13.892893185652));
#103715=CARTESIAN_POINT('Ctrl Pts',(111.469074228514,11.7499598567076,13.9660919690556));
#103716=CARTESIAN_POINT('Ctrl Pts',(111.029469299063,12.0881563461465,14.0026913607574));
#103717=CARTESIAN_POINT('Ctrl Pts',(109.19704085051,12.384596167874,6.50330863924264));
#103718=CARTESIAN_POINT('Ctrl Pts',(108.660050882836,12.1208117444166,6.53990803094444));
#103719=CARTESIAN_POINT('Ctrl Pts',(107.875044890149,11.0271059198285,6.61310681434804));
#103720=CARTESIAN_POINT('Ctrl Pts',(108.595605360236,9.12860131734766,6.72290498945343));
#103721=CARTESIAN_POINT('Ctrl Pts',(110.575553450855,8.68519268703365,6.83270316455883));
#103722=CARTESIAN_POINT('Ctrl Pts',(112.039206579126,10.0883989390783,6.94250133966421));
#103723=CARTESIAN_POINT('Ctrl Pts',(111.677919866503,12.0847248183011,7.05229951476961));
#103724=CARTESIAN_POINT('Ctrl Pts',(109.814327862238,12.8858014143123,7.16209768987499));
#103725=CARTESIAN_POINT('Ctrl Pts',(108.11707347241,11.775151426735,7.27189586498039));
#103726=CARTESIAN_POINT('Ctrl Pts',(108.10532254584,9.74669960984593,7.38169404008578));
#103727=CARTESIAN_POINT('Ctrl Pts',(109.78968731917,8.61643673826731,7.49149221519118));
#103728=CARTESIAN_POINT('Ctrl Pts',(111.662305593259,9.39608090925777,7.60129039029656));
#103729=CARTESIAN_POINT('Ctrl Pts',(112.046861796486,11.3877440490583,7.71108856540196));
#103730=CARTESIAN_POINT('Ctrl Pts',(110.599096307678,12.8085028959323,7.82088674050736));
#103731=CARTESIAN_POINT('Ctrl Pts',(108.615031140635,12.3865257024519,7.93068491561274));
#103732=CARTESIAN_POINT('Ctrl Pts',(107.87076714297,10.4995553393472,8.04048309071814));
#103733=CARTESIAN_POINT('Ctrl Pts',(109.032558892541,8.83677975499,8.15028126582352));
#103734=CARTESIAN_POINT('Ctrl Pts',(111.060388289232,8.8866880898488,8.26007944092893));
#103735=CARTESIAN_POINT('Ctrl Pts',(112.138975095289,10.6046037187379,8.36987761603431));
#103736=CARTESIAN_POINT('Ctrl Pts',(111.302785438136,12.452675696811,8.47967579113971));
#103737=CARTESIAN_POINT('Ctrl Pts',(109.300363047166,12.7765395716466,8.5894739662451));
#103738=CARTESIAN_POINT('Ctrl Pts',(107.924244492418,11.286277502789,8.69927214135049));
#103739=CARTESIAN_POINT('Ctrl Pts',(108.406309188473,9.3159483712207,8.80907031645588));
#103740=CARTESIAN_POINT('Ctrl Pts',(110.315020494028,8.62935939533118,8.91886849156128));
#103741=CARTESIAN_POINT('Ctrl Pts',(111.94173047594,9.84113409006431,9.02866666666666));
#103742=CARTESIAN_POINT('Ctrl Pts',(111.830234284497,11.8665110596832,9.13846484177206));
#103743=CARTESIAN_POINT('Ctrl Pts',(110.080341534207,12.8924051254342,9.24826301687745));
#103744=CARTESIAN_POINT('Ctrl Pts',(108.258528322892,12.0004522706103,9.35806119198285));
#103745=CARTESIAN_POINT('Ctrl Pts',(107.995652799526,9.98911447435552,9.46785936708823));
#103746=CARTESIAN_POINT('Ctrl Pts',(109.5270369425,8.65890927276113,9.57765754219364));
#103747=CARTESIAN_POINT('Ctrl Pts',(111.481810075966,9.20061516012953,9.68745571729902));
#103748=CARTESIAN_POINT('Ctrl Pts',(112.110090448129,11.1293056603398,9.79725389240442));
#103749=CARTESIAN_POINT('Ctrl Pts',(110.849451484067,12.7184477792114,9.9070520675098));
#103750=CARTESIAN_POINT('Ctrl Pts',(108.828397090954,12.5454668214067,10.0168502426152));
#103751=CARTESIAN_POINT('Ctrl Pts',(107.856142947729,10.7652125831984,10.1266484177206));
#103752=CARTESIAN_POINT('Ctrl Pts',(108.803035466554,8.97134028298489,10.236446592826));
#103753=CARTESIAN_POINT('Ctrl Pts',(110.821431557188,8.76969581121582,10.3462447679314));
#103754=CARTESIAN_POINT('Ctrl Pts',(112.104495210703,10.3407880849884,10.4560429430368));
#103755=CARTESIAN_POINT('Ctrl Pts',(111.503648295348,12.2782003426105,10.5658411181422));
#103756=CARTESIAN_POINT('Ctrl Pts',(109.556759392791,12.8475920116615,10.6756392932476));
#103757=CARTESIAN_POINT('Ctrl Pts',(108.006652416955,11.5392527455888,10.7854374683529));
#103758=CARTESIAN_POINT('Ctrl Pts',(108.240958425299,9.52438700164923,10.8952356434583));
#103759=CARTESIAN_POINT('Ctrl Pts',(110.04993041379,8.6066704786518,11.0050338185637));
#103760=CARTESIAN_POINT('Ctrl Pts',(111.814205491688,9.60762838046807,11.1148319936691));
#103761=CARTESIAN_POINT('Ctrl Pts',(111.95443273025,11.6312191476424,11.2246301687745));
#103762=CARTESIAN_POINT('Ctrl Pts',(110.345082940527,12.8659565798388,11.3344283438799));
#103763=CARTESIAN_POINT('Ctrl Pts',(108.426820402868,12.2065234078826,11.4442265189853));
#103764=CARTESIAN_POINT('Ctrl Pts',(107.916843165269,10.2432336974984,11.5540246940907));
#103765=CARTESIAN_POINT('Ctrl Pts',(109.271674722958,8.7335931024099,11.6638228691961));
#103766=CARTESIAN_POINT('Ctrl Pts',(111.278491458847,9.02900782500102,11.7736210443015));
#103767=CARTESIAN_POINT('Ctrl Pts',(112.14082302073,10.8650273061799,11.8834192194069));
#103768=CARTESIAN_POINT('Ctrl Pts',(111.086723933259,12.5980761873106,11.9932173945123));
#103769=CARTESIAN_POINT('Ctrl Pts',(109.059806910231,12.6767566998151,12.1030155696177));
#103770=CARTESIAN_POINT('Ctrl Pts',(107.874535738854,11.0306353710037,12.2128137447231));
#103771=CARTESIAN_POINT('Ctrl Pts',(108.591946329617,9.13329363835785,12.3226119198284));
#103772=CARTESIAN_POINT('Ctrl Pts',(110.569824054753,8.68320186062037,12.4324100949338));
#103773=CARTESIAN_POINT('Ctrl Pts',(112.037604507435,10.0832744501776,12.5422082700392));
#103774=CARTESIAN_POINT('Ctrl Pts',(111.681353600035,12.0801899066839,12.6520064451446));
#103775=CARTESIAN_POINT('Ctrl Pts',(109.819982324182,12.8863389700205,12.76180462025));
#103776=CARTESIAN_POINT('Ctrl Pts',(108.119758832288,11.7800746755757,12.8716027953554));
#103777=CARTESIAN_POINT('Ctrl Pts',(108.102699645371,9.75169736352991,12.9814009704608));
#103778=CARTESIAN_POINT('Ctrl Pts',(109.784068649759,8.61699806199891,13.0911991455662));
#103779=CARTESIAN_POINT('Ctrl Pts',(111.658745815704,9.39170082563866,13.2009973206716));
#103780=CARTESIAN_POINT('Ctrl Pts',(112.048520105805,11.3823868532413,13.310795495777));
#103781=CARTESIAN_POINT('Ctrl Pts',(110.604532668541,12.8068573301973,13.4205936708824));
#103782=CARTESIAN_POINT('Ctrl Pts',(108.619294160841,12.3902916828128,13.5303918459878));
#103783=CARTESIAN_POINT('Ctrl Pts',(107.870210523387,10.5048954886742,13.6401900210931));
#103784=CARTESIAN_POINT('Ctrl Pts',(109.027336582184,8.83986469324491,13.7499881961986));
#103785=CARTESIAN_POINT('Ctrl Pts',(111.055873284095,8.88281238215351,13.8597863713039));
#103786=CARTESIAN_POINT('Ctrl Pts',(112.137777768013,10.6012447504384,13.9695845464093));
#103787=CARTESIAN_POINT('Ctrl Pts',(111.584656870185,11.8286338947921,14.0427833298129));
#103788=CARTESIAN_POINT('Ctrl Pts',(111.11046505734,12.193438735868,14.0793827215147));
#103789=CARTESIAN_POINT('Ctrl Pts',(109.13847414033,12.5038213116276,6.58));
#103790=CARTESIAN_POINT('Ctrl Pts',(108.562316880239,12.2207968236057,6.6165993917018));
#103791=CARTESIAN_POINT('Ctrl Pts',(107.720053655359,11.0473176355879,6.68979817510539));
#103792=CARTESIAN_POINT('Ctrl Pts',(108.493170791929,9.01033877959037,6.79959635021078));
#103793=CARTESIAN_POINT('Ctrl Pts',(110.617533509456,8.53458854788894,6.90939452531619));
#103794=CARTESIAN_POINT('Ctrl Pts',(112.187943436778,10.0401426889131,7.01919270042156));
#103795=CARTESIAN_POINT('Ctrl Pts',(111.800304979855,12.1820777678926,7.12899087552697));
#103796=CARTESIAN_POINT('Ctrl Pts',(109.800785197847,13.0415837632834,7.23878905063235));
#103797=CARTESIAN_POINT('Ctrl Pts',(107.979735461749,11.8499245288773,7.34858722573775));
#103798=CARTESIAN_POINT('Ctrl Pts',(107.967127439135,9.67352029155613,7.45838540084314));
#103799=CARTESIAN_POINT('Ctrl Pts',(109.77434740825,8.46081763699515,7.56818357594853));
#103800=CARTESIAN_POINT('Ctrl Pts',(111.783551823499,9.29732795645082,7.67798175105392));
#103801=CARTESIAN_POINT('Ctrl Pts',(112.196157014917,11.4342602023574,7.78777992615932));
#103802=CARTESIAN_POINT('Ctrl Pts',(110.642793549118,12.9586471997721,7.89757810126471));
#103803=CARTESIAN_POINT('Ctrl Pts',(108.514013461408,12.5058915837418,8.0073762763701));
#103804=CARTESIAN_POINT('Ctrl Pts',(107.715463895321,10.4812882583057,8.11717445147549));
#103805=CARTESIAN_POINT('Ctrl Pts',(108.961995099858,8.69723216321981,8.22697262658088));
#103806=CARTESIAN_POINT('Ctrl Pts',(111.137731518528,8.75078074177608,8.33677080168628));
#103807=CARTESIAN_POINT('Ctrl Pts',(112.294988928083,10.5939987186312,8.44656897679166));
#103808=CARTESIAN_POINT('Ctrl Pts',(111.397808774294,12.5768664655818,8.55636715189706));
#103809=CARTESIAN_POINT('Ctrl Pts',(109.249332512581,12.9243525156022,8.66616532700245));
#103810=CARTESIAN_POINT('Ctrl Pts',(107.772841807367,11.3253928290197,8.77596350210785));
#103811=CARTESIAN_POINT('Ctrl Pts',(108.290067623836,9.2113506638777,8.88576167721323));
#103812=CARTESIAN_POINT('Ctrl Pts',(110.337997645464,8.47468285447632,8.99555985231864));
#103813=CARTESIAN_POINT('Ctrl Pts',(112.083357563825,9.77484268984296,9.10535802742402));
#103814=CARTESIAN_POINT('Ctrl Pts',(111.963728997112,11.9479478048619,9.21515620252942));
#103815=CARTESIAN_POINT('Ctrl Pts',(110.086201532629,13.0486691397997,9.3249543776348));
#103816=CARTESIAN_POINT('Ctrl Pts',(108.131507829924,12.0916584991887,9.43475255274021));
#103817=CARTESIAN_POINT('Ctrl Pts',(107.849458535887,9.93361655507863,9.54455072784558));
#103818=CARTESIAN_POINT('Ctrl Pts',(109.492539682792,8.5063880583739,9.65434890295099));
#103819=CARTESIAN_POINT('Ctrl Pts',(111.589891217225,9.08760521070363,9.76414707805638));
#103820=CARTESIAN_POINT('Ctrl Pts',(112.263997475416,11.1569716813237,9.87394525316177));
#103821=CARTESIAN_POINT('Ctrl Pts',(110.911409279692,12.8620235895922,9.98374342826716));
#103822=CARTESIAN_POINT('Ctrl Pts',(108.742942023825,12.6764256441999,10.0935416033726));
#103823=CARTESIAN_POINT('Ctrl Pts',(107.699773031864,10.7663221676049,10.2033397784779));
#103824=CARTESIAN_POINT('Ctrl Pts',(108.715730558239,8.84160734672965,10.3131379535833));
#103825=CARTESIAN_POINT('Ctrl Pts',(110.881345618785,8.6252552110089,10.4229361286887));
#103826=CARTESIAN_POINT('Ctrl Pts',(112.257994129247,10.3109407438825,10.5327343037941));
#103827=CARTESIAN_POINT('Ctrl Pts',(111.613322285592,12.3896651246239,10.6425324788995));
#103828=CARTESIAN_POINT('Ctrl Pts',(109.524430046773,13.0005874205838,10.7523306540049));
#103829=CARTESIAN_POINT('Ctrl Pts',(107.861260449929,11.596819729961,10.8621288291103));
#103830=CARTESIAN_POINT('Ctrl Pts',(108.112656408731,9.43499251462759,10.9719270042157));
#103831=CARTESIAN_POINT('Ctrl Pts',(110.053572267893,8.45033904014951,11.0817251793211));
#103832=CARTESIAN_POINT('Ctrl Pts',(111.946531086717,9.52430540245334,11.1915233544265));
#103833=CARTESIAN_POINT('Ctrl Pts',(112.096986302686,11.6954940319355,11.3013215295319));
#103834=CARTESIAN_POINT('Ctrl Pts',(110.370252804496,13.0202914745154,11.4111197046373));
#103835=CARTESIAN_POINT('Ctrl Pts',(108.312074897339,12.3127601751638,11.5209178797427));
#103836=CARTESIAN_POINT('Ctrl Pts',(107.764900637834,10.206270876679,11.630716054848));
#103837=CARTESIAN_POINT('Ctrl Pts',(109.218551702385,8.58651922143807,11.7405142299534));
#103838=CARTESIAN_POINT('Ctrl Pts',(111.371742826349,8.90348107809205,11.8503124050588));
#103839=CARTESIAN_POINT('Ctrl Pts',(112.296971638605,10.8734172359891,11.9601105801642));
#103840=CARTESIAN_POINT('Ctrl Pts',(111.165988047362,12.7328722632039,12.0699087552696));
#103841=CARTESIAN_POINT('Ctrl Pts',(108.991230549607,12.8172916215459,12.179706930375));
#103842=CARTESIAN_POINT('Ctrl Pts',(107.719507367285,11.0511045199641,12.2895051054804));
#103843=CARTESIAN_POINT('Ctrl Pts',(108.489244876767,9.01537335189051,12.3993032805858));
#103844=CARTESIAN_POINT('Ctrl Pts',(110.611386219267,8.5324525133992,12.5091014556912));
#103845=CARTESIAN_POINT('Ctrl Pts',(112.186224512233,10.0346444270048,12.6188996307966));
#103846=CARTESIAN_POINT('Ctrl Pts',(111.803989165079,12.177212086205,12.728697805902));
#103847=CARTESIAN_POINT('Ctrl Pts',(109.806852088287,13.0421605275483,12.8384959810074));
#103848=CARTESIAN_POINT('Ctrl Pts',(107.982616687997,11.8552068725587,12.9482941561128));
#103849=CARTESIAN_POINT('Ctrl Pts',(107.964313227998,9.67888257435937,13.0580923312181));
#103850=CARTESIAN_POINT('Ctrl Pts',(109.768318921001,8.46141990288965,13.1678905063235));
#103851=CARTESIAN_POINT('Ctrl Pts',(111.779732400779,9.29262839569759,13.2776886814289));
#103852=CARTESIAN_POINT('Ctrl Pts',(112.197936278984,11.4285122602179,13.3874868565343));
#103853=CARTESIAN_POINT('Ctrl Pts',(110.648626430491,12.9568816087886,13.4972850316397));
#103854=CARTESIAN_POINT('Ctrl Pts',(108.518587420307,12.5099322494094,13.6070832067451));
#103855=CARTESIAN_POINT('Ctrl Pts',(107.71486667669,10.4870179106083,13.7168813818505));
#103856=CARTESIAN_POINT('Ctrl Pts',(108.956391881534,8.70054211252889,13.8266795569559));
#103857=CARTESIAN_POINT('Ctrl Pts',(111.132887195271,8.74662234541666,13.9364777320613));
#103858=CARTESIAN_POINT('Ctrl Pts',(112.293704269442,10.5903947519117,14.0462759071667));
#103859=CARTESIAN_POINT('Ctrl Pts',(111.700239511856,11.9073079328766,14.1194746905703));
#103860=CARTESIAN_POINT('Ctrl Pts',(111.191460815618,12.2987211255895,14.1560740822721));
#103861=CARTESIAN_POINT('Ctrl Pts',(108.043923528227,10.7487415210877,13.7041303078758));
#103862=CARTESIAN_POINT('Ctrl Pts',(108.043390553338,10.6744197365054,13.7083806658673));
#103863=CARTESIAN_POINT('Ctrl Pts',(108.047267155266,10.600156305453,13.7126310238589));
#103864=CARTESIAN_POINT('Ctrl Pts',(108.055741001433,10.5264243340619,13.7168813818505));
#103865=CARTESIAN_POINT('Ctrl Pts',(108.128708411638,9.89152597791513,13.7534807735523));
#103866=CARTESIAN_POINT('Ctrl Pts',(108.542550146586,9.29603404522202,13.7900801652541));
#103867=CARTESIAN_POINT('Ctrl Pts',(109.112220233016,9.00596811769008,13.8266795569559));
#103868=CARTESIAN_POINT('Ctrl Pts',(109.627528300012,8.74358236850237,13.8597863713039));
#103869=CARTESIAN_POINT('Ctrl Pts',(110.27034322046,8.73111204555335,13.892893185652));
#103870=CARTESIAN_POINT('Ctrl Pts',(110.800030261768,8.96425629420689,13.926));
#103871=CARTESIAN_POINT('',(109.094485737464,9.48253146637784,6.58));
#103872=CARTESIAN_POINT('Ctrl Pts',(109.094485737464,9.48253146637783,6.58));
#103873=CARTESIAN_POINT('Ctrl Pts',(109.050936912807,9.50575319919841,6.58));
#103874=CARTESIAN_POINT('Ctrl Pts',(109.008665973235,9.53109748968633,6.58));
#103875=CARTESIAN_POINT('Ctrl Pts',(108.967849928603,9.55852424242646,6.58));
#103876=CARTESIAN_POINT('Ctrl Pts',(108.918405134776,9.59174917019158,6.58));
#103877=CARTESIAN_POINT('Ctrl Pts',(108.87109400725,9.62802846914193,6.58));
#103878=CARTESIAN_POINT('Ctrl Pts',(108.825992689794,9.66704649021906,6.58));
#103879=CARTESIAN_POINT('Ctrl Pts',(108.811269067091,9.67978418067566,6.58));
#103880=CARTESIAN_POINT('Ctrl Pts',(108.796781101392,9.6928141355179,6.58));
#103881=CARTESIAN_POINT('Ctrl Pts',(108.782531922016,9.70612644259636,6.58));
#103882=CARTESIAN_POINT('Ctrl Pts',(108.768136779111,9.71957511621697,6.58));
#103883=CARTESIAN_POINT('Ctrl Pts',(108.753980780056,9.73331684541932,6.58));
#103884=CARTESIAN_POINT('Ctrl Pts',(108.740092740145,9.74731551635198,6.58));
#103885=CARTESIAN_POINT('Ctrl Pts',(108.696277375476,9.7914799107319,6.58));
#103886=CARTESIAN_POINT('Ctrl Pts',(108.655087119634,9.83823222524873,6.58));
#103887=CARTESIAN_POINT('Ctrl Pts',(108.616602456003,9.88722312609965,6.58));
#103888=CARTESIAN_POINT('Ctrl Pts',(108.586435257704,9.92562590999792,6.58));
#103889=CARTESIAN_POINT('Ctrl Pts',(108.557930796962,9.96540544741069,6.58));
#103890=CARTESIAN_POINT('Ctrl Pts',(108.531138759219,10.006412957565,6.58));
#103891=CARTESIAN_POINT('Ctrl Pts',(108.519242344837,10.024621439436,6.58));
#103892=CARTESIAN_POINT('Ctrl Pts',(108.507683697692,10.0430722310019,6.58));
#103893=CARTESIAN_POINT('Ctrl Pts',(108.496467920523,10.0617531902008,6.58));
#103894=CARTESIAN_POINT('Ctrl Pts',(108.489773727828,10.0729030141253,6.58));
#103895=CARTESIAN_POINT('Ctrl Pts',(108.483205613724,10.0841284017624,6.58));
#103896=CARTESIAN_POINT('Ctrl Pts',(108.476767613657,10.0954204877901,6.58));
#103897=CARTESIAN_POINT('Ctrl Pts',(108.444738154717,10.1515993324623,6.58));
#103898=CARTESIAN_POINT('Ctrl Pts',(108.415900039582,10.2094701677432,6.58));
#103899=CARTESIAN_POINT('Ctrl Pts',(108.390338629852,10.2686792144268,6.58));
#103900=CARTESIAN_POINT('Ctrl Pts',(108.364258095986,10.3290907317699,6.58));
#103901=CARTESIAN_POINT('Ctrl Pts',(108.341587974258,10.3908961572324,6.58));
#103902=CARTESIAN_POINT('Ctrl Pts',(108.32245351373,10.4537607571801,6.58));
#103903=CARTESIAN_POINT('Ctrl Pts',(108.30955567597,10.4961354773764,6.58));
#103904=CARTESIAN_POINT('Ctrl Pts',(108.298265032162,10.5389922949493,6.58));
#103905=CARTESIAN_POINT('Ctrl Pts',(108.288631134875,10.5822359881016,6.58));
#103906=CARTESIAN_POINT('Ctrl Pts',(108.281989541746,10.6120481198671,6.58));
#103907=CARTESIAN_POINT('Ctrl Pts',(108.276135541372,10.6420442390975,6.58));
#103908=CARTESIAN_POINT('Ctrl Pts',(108.271088271902,10.672194168098,6.58));
#103909=CARTESIAN_POINT('Ctrl Pts',(108.269449801862,10.6819815899274,6.58));
#103910=CARTESIAN_POINT('Ctrl Pts',(108.267896731562,10.6917833667726,6.58));
#103911=CARTESIAN_POINT('Ctrl Pts',(108.266430872539,10.7015893700294,6.58));
#103912=CARTESIAN_POINT('Ctrl Pts',(108.256410853655,10.7686192386944,6.58));
#103913=CARTESIAN_POINT('Ctrl Pts',(108.250442320048,10.8359619127518,6.58));
#103914=CARTESIAN_POINT('Ctrl Pts',(108.248640216193,10.9032609407739,6.58));
#103915=CARTESIAN_POINT('Ctrl Pts',(108.247984029468,10.9277660372508,6.58));
#103916=CARTESIAN_POINT('Ctrl Pts',(108.247880654352,10.9522656427428,6.58));
#103917=CARTESIAN_POINT('Ctrl Pts',(108.248337121755,10.9767434152174,6.58));
#103918=CARTESIAN_POINT('Ctrl Pts',(108.249548986487,11.0417288862322,6.58));
#103919=CARTESIAN_POINT('Ctrl Pts',(108.254702968127,11.1065599084768,6.58));
#103920=CARTESIAN_POINT('Ctrl Pts',(108.263584862996,11.1710011132196,6.58));
#103921=CARTESIAN_POINT('Ctrl Pts',(108.268229471318,11.2046993454291,6.58));
#103922=CARTESIAN_POINT('Ctrl Pts',(108.273894368221,11.2382911384497,6.58));
#103923=CARTESIAN_POINT('Ctrl Pts',(108.280554427054,11.2717432628227,6.58));
#103924=CARTESIAN_POINT('Ctrl Pts',(108.283902653934,11.2885607271757,6.58));
#103925=CARTESIAN_POINT('Ctrl Pts',(108.287502455648,11.3053428915284,6.58));
#103926=CARTESIAN_POINT('Ctrl Pts',(108.291350983268,11.3220855124536,6.58));
#103927=CARTESIAN_POINT('Ctrl Pts',(108.294074929971,11.3339357605395,6.58));
#103928=CARTESIAN_POINT('Ctrl Pts',(108.296923840734,11.3457676088853,6.58));
#103929=CARTESIAN_POINT('Ctrl Pts',(108.299895665582,11.3575751561644,6.58));
#103930=CARTESIAN_POINT('Ctrl Pts',(108.316402383052,11.4231590505621,6.58));
#103931=CARTESIAN_POINT('Ctrl Pts',(108.33662697865,11.4877187759529,6.58));
#103932=CARTESIAN_POINT('Ctrl Pts',(108.360307162796,11.5510007167747,6.58));
#103933=CARTESIAN_POINT('Ctrl Pts',(108.384511690055,11.6156838903606,6.58));
#103934=CARTESIAN_POINT('Ctrl Pts',(108.412326689962,11.6790329257557,6.58));
#103935=CARTESIAN_POINT('Ctrl Pts',(108.443527431511,11.7407814451632,6.58));
#103936=CARTESIAN_POINT('Ctrl Pts',(108.475025086212,11.8031175771291,6.58));
#103937=CARTESIAN_POINT('Ctrl Pts',(108.509973535022,11.8638235615249,6.58));
#103938=CARTESIAN_POINT('Ctrl Pts',(108.548193675815,11.9226158531736,6.58));
#103939=CARTESIAN_POINT('Ctrl Pts',(108.563444783309,11.9460759331508,6.58));
#103940=CARTESIAN_POINT('Ctrl Pts',(108.579217385883,11.9692311139236,6.58));
#103941=CARTESIAN_POINT('Ctrl Pts',(108.595502214161,11.9920624177307,6.58));
#103942=CARTESIAN_POINT('Ctrl Pts',(108.601528527372,12.0005112994394,6.58));
#103943=CARTESIAN_POINT('Ctrl Pts',(108.607623934891,12.0089142481693,6.58));
#103944=CARTESIAN_POINT('Ctrl Pts',(108.613782347307,12.0172630060722,6.58));
#103945=CARTESIAN_POINT('Ctrl Pts',(108.656623913337,12.0753419132332,6.58));
#103946=CARTESIAN_POINT('Ctrl Pts',(108.702582196294,12.1309004454991,6.58));
#103947=CARTESIAN_POINT('Ctrl Pts',(108.751414460567,12.1836589933253,6.58));
#103948=CARTESIAN_POINT('Ctrl Pts',(108.800370406047,12.2365511667563,6.58));
#103949=CARTESIAN_POINT('Ctrl Pts',(108.852215343132,12.2866301616735,6.58));
#103950=CARTESIAN_POINT('Ctrl Pts',(108.906754319057,12.3335980072095,6.58));
#103951=CARTESIAN_POINT('Ctrl Pts',(108.960144301937,12.3795763635418,6.58));
#103952=CARTESIAN_POINT('Ctrl Pts',(109.016116578056,12.4225741338096,6.58));
#103953=CARTESIAN_POINT('Ctrl Pts',(109.074528046071,12.4622826185796,6.58));
#103954=CARTESIAN_POINT('Ctrl Pts',(109.095529607657,12.4765596127507,6.58));
#103955=CARTESIAN_POINT('Ctrl Pts',(109.116846828723,12.490411052127,6.58));
#103956=CARTESIAN_POINT('Ctrl Pts',(109.138474140329,12.5038213116275,6.58));
#103957=CARTESIAN_POINT('Ctrl Pts',(109.094485737464,9.48253146637784,6.58));
#103958=CARTESIAN_POINT('Ctrl Pts',(109.471097310481,9.21718459007931,6.61310681434804));
#103959=CARTESIAN_POINT('Ctrl Pts',(110.531359103967,9.02452446360541,6.68281302039787));
#103960=CARTESIAN_POINT('Ctrl Pts',(111.741732863822,10.1849114394086,6.7891186181495));
#103961=CARTESIAN_POINT('Ctrl Pts',(111.433149639798,11.8900189191182,6.8989167932549));
#103962=CARTESIAN_POINT('Ctrl Pts',(109.841413191019,12.5742367163702,7.00871496836029));
#103963=CARTESIAN_POINT('Ctrl Pts',(108.630525892921,11.7818558153983,7.10042811247656));
#103964=CARTESIAN_POINT('Ctrl Pts',(108.446950083986,11.0094136788633,7.15554186489103));
#103965=CARTESIAN_POINT('Ctrl Pts',(108.446877037961,10.7499579969204,7.17405622560371));
#103966=CARTESIAN_POINT('Origin',(110.,10.75,6.58));
#103967=CARTESIAN_POINT('',(108.046,10.75,6.58));
#103968=CARTESIAN_POINT('Origin',(110.,10.75,6.58));
#103969=CARTESIAN_POINT('',(110.90360677865,9.48387400327716,6.58));
#103970=CARTESIAN_POINT('Ctrl Pts',(110.863615890953,12.505874778859,6.58));
#103971=CARTESIAN_POINT('Ctrl Pts',(110.91572812803,12.4739601120705,6.58));
#103972=CARTESIAN_POINT('Ctrl Pts',(110.966139416693,12.439530981949,6.58));
#103973=CARTESIAN_POINT('Ctrl Pts',(111.014633065925,12.4025819390746,6.58));
#103974=CARTESIAN_POINT('Ctrl Pts',(111.071887742848,12.3589575563801,6.58));
#103975=CARTESIAN_POINT('Ctrl Pts',(111.126470551244,12.3118203447527,6.58));
#103976=CARTESIAN_POINT('Ctrl Pts',(111.178217601733,12.2615103151031,6.58));
#103977=CARTESIAN_POINT('Ctrl Pts',(111.200555824445,12.2397924271013,6.58));
#103978=CARTESIAN_POINT('Ctrl Pts',(111.22236504181,12.217482947574,6.58));
#103979=CARTESIAN_POINT('Ctrl Pts',(111.243629369983,12.1946080117045,6.58));
#103980=CARTESIAN_POINT('Ctrl Pts',(111.253927421759,12.1835299624928,6.58));
#103981=CARTESIAN_POINT('Ctrl Pts',(111.264098257918,12.1723184344817,6.58));
#103982=CARTESIAN_POINT('Ctrl Pts',(111.274128934465,12.160989281423,6.58));
#103983=CARTESIAN_POINT('Ctrl Pts',(111.321394235603,12.1076054614567,6.58));
#103984=CARTESIAN_POINT('Ctrl Pts',(111.365611705757,12.0515482090722,6.58));
#103985=CARTESIAN_POINT('Ctrl Pts',(111.406629229378,11.993155953854,6.58));
#103986=CARTESIAN_POINT('Ctrl Pts',(111.436793500335,11.9502143120222,6.58));
#103987=CARTESIAN_POINT('Ctrl Pts',(111.465226304169,11.9060091415309,6.58));
#103988=CARTESIAN_POINT('Ctrl Pts',(111.491850087055,11.8606693411838,6.58));
#103989=CARTESIAN_POINT('Ctrl Pts',(111.505971478861,11.836620877153,6.58));
#103990=CARTESIAN_POINT('Ctrl Pts',(111.519583686763,11.812253154722,6.58));
#103991=CARTESIAN_POINT('Ctrl Pts',(111.532673360189,11.7875852440055,6.58));
#103992=CARTESIAN_POINT('Ctrl Pts',(111.538699343551,11.7762290844812,6.58));
#103993=CARTESIAN_POINT('Ctrl Pts',(111.544615248108,11.7648077886736,6.58));
#103994=CARTESIAN_POINT('Ctrl Pts',(111.550412449506,11.7533380324003,6.58));
#103995=CARTESIAN_POINT('Ctrl Pts',(111.581821459515,11.6911953423588,6.58));
#103996=CARTESIAN_POINT('Ctrl Pts',(111.609799978483,11.6275397259463,6.58));
#103997=CARTESIAN_POINT('Ctrl Pts',(111.634204607343,11.5626834155388,6.58));
#103998=CARTESIAN_POINT('Ctrl Pts',(111.658058374836,11.4992910419925,6.58));
#103999=CARTESIAN_POINT('Ctrl Pts',(111.678497866089,11.4347505754478,6.58));
#104000=CARTESIAN_POINT('Ctrl Pts',(111.695340844405,11.3693475318887,6.58));
#104001=CARTESIAN_POINT('Ctrl Pts',(111.707094266335,11.3237077672309,6.58));
#104002=CARTESIAN_POINT('Ctrl Pts',(111.717095347781,11.2776478329959,6.58));
#104003=CARTESIAN_POINT('Ctrl Pts',(111.725267312939,11.2312666793572,6.58));
#104004=CARTESIAN_POINT('Ctrl Pts',(111.732144455438,11.1922344763675,6.58));
#104005=CARTESIAN_POINT('Ctrl Pts',(111.737725998123,11.152974769157,6.58));
#104006=CARTESIAN_POINT('Ctrl Pts',(111.741959093489,11.1135487316366,6.58));
#104007=CARTESIAN_POINT('Ctrl Pts',(111.743158992768,11.1023731568108,6.58));
#104008=CARTESIAN_POINT('Ctrl Pts',(111.744250311734,11.0911852598384,6.58));
#104009=CARTESIAN_POINT('Ctrl Pts',(111.74523093843,11.0799993039966,6.58));
#104010=CARTESIAN_POINT('Ctrl Pts',(111.750925211886,11.0150450337225,6.58));
#104011=CARTESIAN_POINT('Ctrl Pts',(111.752904211648,10.9500399141499,6.58));
#104012=CARTESIAN_POINT('Ctrl Pts',(111.751006925574,10.8852470369328,6.58));
#104013=CARTESIAN_POINT('Ctrl Pts',(111.750274493205,10.8602342561979,6.58));
#104014=CARTESIAN_POINT('Ctrl Pts',(111.74896384625,10.8352531697528,6.58));
#104015=CARTESIAN_POINT('Ctrl Pts',(111.747063655824,10.8103193158065,6.58));
#104016=CARTESIAN_POINT('Ctrl Pts',(111.741910029986,10.7426946440209,6.58));
#104017=CARTESIAN_POINT('Ctrl Pts',(111.732423328962,10.6754153544111,6.58));
#104018=CARTESIAN_POINT('Ctrl Pts',(111.718786593378,10.6088083758369,6.58));
#104019=CARTESIAN_POINT('Ctrl Pts',(111.712609441295,10.5786368267949,6.58));
#104020=CARTESIAN_POINT('Ctrl Pts',(111.705580063643,10.5486036087976,6.58));
#104021=CARTESIAN_POINT('Ctrl Pts',(111.697712407598,10.518741398877,6.58));
#104022=CARTESIAN_POINT('Ctrl Pts',(111.692759526394,10.49994241003,6.58));
#104023=CARTESIAN_POINT('Ctrl Pts',(111.687474399047,10.4812112234672,6.58));
#104024=CARTESIAN_POINT('Ctrl Pts',(111.681860175243,10.4625563565017,6.58));
#104025=CARTESIAN_POINT('Ctrl Pts',(111.677548653405,10.4482300900213,6.58));
#104026=CARTESIAN_POINT('Ctrl Pts',(111.673041469894,10.433944527391,6.58));
#104027=CARTESIAN_POINT('Ctrl Pts',(111.668349447529,10.4197311039683,6.58));
#104028=CARTESIAN_POINT('Ctrl Pts',(111.648040497254,10.358209719986,6.58));
#104029=CARTESIAN_POINT('Ctrl Pts',(111.624246746503,10.2979449974984,6.58));
#104030=CARTESIAN_POINT('Ctrl Pts',(111.597157677967,10.239209273296,6.58));
#104031=CARTESIAN_POINT('Ctrl Pts',(111.570152434372,10.1806553020634,6.58));
#104032=CARTESIAN_POINT('Ctrl Pts',(111.53987147901,10.1236200399665,6.58));
#104033=CARTESIAN_POINT('Ctrl Pts',(111.506462520857,10.0684054610765,6.58));
#104034=CARTESIAN_POINT('Ctrl Pts',(111.473719317685,10.0142911673477,6.58));
#104035=CARTESIAN_POINT('Ctrl Pts',(111.43797078304,9.96192508876454,6.58));
#104036=CARTESIAN_POINT('Ctrl Pts',(111.399328735281,9.91163309421039,6.58));
#104037=CARTESIAN_POINT('Ctrl Pts',(111.390569611906,9.90023323807856,6.58));
#104038=CARTESIAN_POINT('Ctrl Pts',(111.381661730486,9.88894014350557,6.58));
#104039=CARTESIAN_POINT('Ctrl Pts',(111.372606253593,9.87775796120325,6.58));
#104040=CARTESIAN_POINT('Ctrl Pts',(111.365851060438,9.86941629104745,6.58));
#104041=CARTESIAN_POINT('Ctrl Pts',(111.359019323853,9.86114327231143,6.58));
#104042=CARTESIAN_POINT('Ctrl Pts',(111.352113301533,9.852941945223,6.58));
#104043=CARTESIAN_POINT('Ctrl Pts',(111.312156197831,9.80549042222458,6.58));
#104044=CARTESIAN_POINT('Ctrl Pts',(111.269699060544,9.76041611218175,6.58));
#104045=CARTESIAN_POINT('Ctrl Pts',(111.224881640097,9.71798642199737,6.58));
#104046=CARTESIAN_POINT('Ctrl Pts',(111.180871242947,9.67632075946335,6.58));
#104047=CARTESIAN_POINT('Ctrl Pts',(111.134584090894,9.63720479812122,6.58));
#104048=CARTESIAN_POINT('Ctrl Pts',(111.08612936571,9.60093579887304,6.58));
#104049=CARTESIAN_POINT('Ctrl Pts',(111.039216000705,9.56582052799681,6.58));
#104050=CARTESIAN_POINT('Ctrl Pts',(110.990270163602,9.53337367842178,6.58));
#104051=CARTESIAN_POINT('Ctrl Pts',(110.93937862246,9.50391249752929,6.58));
#104052=CARTESIAN_POINT('Ctrl Pts',(110.927559307518,9.49707028038017,6.58));
#104053=CARTESIAN_POINT('Ctrl Pts',(110.915635013035,9.49038932175318,6.58));
#104054=CARTESIAN_POINT('Ctrl Pts',(110.90360677865,9.48387400327717,6.58));
#104055=CARTESIAN_POINT('Origin',(110.,10.75,6.58));
#104056=CARTESIAN_POINT('Origin',(110.,10.75,6.58));
#104057=CARTESIAN_POINT('Origin',(110.,10.75,5.2859437743963));
#104058=CARTESIAN_POINT('Ctrl Pts',(110.90360677865,9.48387400327716,6.58));
#104059=CARTESIAN_POINT('Ctrl Pts',(111.319548631087,9.78072272003922,6.6165993917018));
#104060=CARTESIAN_POINT('Ctrl Pts',(111.829309884247,10.8114276571461,6.68979817510539));
#104061=CARTESIAN_POINT('Ctrl Pts',(110.958511260717,12.3114074675171,6.79959635021079));
#104062=CARTESIAN_POINT('Ctrl Pts',(109.228325960441,12.4102596813202,6.90939452531617));
#104063=CARTESIAN_POINT('Ctrl Pts',(108.483008121587,11.4159579759326,6.98817700004468));
#104064=CARTESIAN_POINT('Ctrl Pts',(108.44267854523,10.8289870709956,7.03036008307139));
#104065=CARTESIAN_POINT('Ctrl Pts',(108.443317976897,10.7511999786121,7.0359437743963));
#104066=CARTESIAN_POINT('Ctrl Pts',(111.135099739944,9.15950806969049,6.34992591772793));
#104067=CARTESIAN_POINT('Ctrl Pts',(111.657600787621,9.53240578267863,6.38652530942973));
#104068=CARTESIAN_POINT('Ctrl Pts',(112.297956614477,10.8271646686361,6.45972409283333));
#104069=CARTESIAN_POINT('Ctrl Pts',(111.204070076144,12.7114208881571,6.56952226793872));
#104070=CARTESIAN_POINT('Ctrl Pts',(109.030632546899,12.8355978253293,6.67932044304411));
#104071=CARTESIAN_POINT('Ctrl Pts',(107.725779622808,11.0948404999723,6.7891186181495));
#104072=CARTESIAN_POINT('Ctrl Pts',(108.45636747918,9.04437908018243,6.8989167932549));
#104073=CARTESIAN_POINT('Ctrl Pts',(110.568989660983,8.52125780622274,7.00871496836028));
#104074=CARTESIAN_POINT('Ctrl Pts',(112.172163502637,9.99302748812491,7.11851314346568));
#104075=CARTESIAN_POINT('Ctrl Pts',(111.830899302783,12.1425466001077,7.22831131857107));
#104076=CARTESIAN_POINT('Ctrl Pts',(109.850619585433,13.0454213538711,7.33810949367646));
#104077=CARTESIAN_POINT('Ctrl Pts',(108.004074456252,11.893500419209,7.44790766878186));
#104078=CARTESIAN_POINT('Ctrl Pts',(107.944244347984,9.71792192022829,7.55770584388725));
#104079=CARTESIAN_POINT('Ctrl Pts',(109.72469674044,8.46625025519251,7.66750401899264));
#104080=CARTESIAN_POINT('Ctrl Pts',(111.751594842584,9.2589515263096,7.77730219409804));
#104081=CARTESIAN_POINT('Ctrl Pts',(112.21049383889,11.3864173132724,7.88710036920343));
#104082=CARTESIAN_POINT('Ctrl Pts',(110.690593650437,12.9441716355246,7.99689854430882));
#104083=CARTESIAN_POINT('Ctrl Pts',(108.552485197456,12.5377388906333,8.1066967194142));
#104084=CARTESIAN_POINT('Ctrl Pts',(107.710168843071,10.5309505853093,8.21649489451961));
#104085=CARTESIAN_POINT('Ctrl Pts',(108.91767288213,8.72025192310877,8.326293069625));
#104086=CARTESIAN_POINT('Ctrl Pts',(111.094058886326,8.72655133855564,8.43609124473038));
#104087=CARTESIAN_POINT('Ctrl Pts',(112.29106082336,10.5442097675935,8.54588941983578));
#104088=CARTESIAN_POINT('Ctrl Pts',(111.437141624057,12.5460883208689,8.65568759494117));
#104089=CARTESIAN_POINT('Ctrl Pts',(109.296716151948,12.9401372430785,8.76548577004656));
#104090=CARTESIAN_POINT('Ctrl Pts',(107.78585916977,11.3736102112643,8.87528394515196));
#104091=CARTESIAN_POINT('Ctrl Pts',(108.25706576797,9.2488372594989,8.98508212025735));
#104092=CARTESIAN_POINT('Ctrl Pts',(110.288519309612,8.46788126517022,9.09488029536274));
#104093=CARTESIAN_POINT('Ctrl Pts',(112.061694964162,9.72984158768768,9.20467847046813));
#104094=CARTESIAN_POINT('Ctrl Pts',(111.989274148281,11.9050314603394,9.31447664557353));
#104095=CARTESIAN_POINT('Ctrl Pts',(110.136086822123,13.0462555799335,9.42427482067892));
#104096=CARTESIAN_POINT('Ctrl Pts',(108.161076741885,12.1319083045691,9.53407299578431));
#104097=CARTESIAN_POINT('Ctrl Pts',(107.832241451546,9.98049874134283,9.64387117088971));
#104098=CARTESIAN_POINT('Ctrl Pts',(109.443949061668,8.51793443970259,9.75366934599509));
#104099=CARTESIAN_POINT('Ctrl Pts',(111.553424608837,9.05347965053842,9.86346752110049));
#104100=CARTESIAN_POINT('Ctrl Pts',(112.272299206359,11.1077228372095,9.97326569620588));
#104101=CARTESIAN_POINT('Ctrl Pts',(110.957047772743,12.8417382417903,10.0830638713113));
#104102=CARTESIAN_POINT('Ctrl Pts',(108.785062427444,12.7032629127364,10.1928620464167));
#104103=CARTESIAN_POINT('Ctrl Pts',(107.700669832091,10.8162577574453,10.3026602215221));
#104104=CARTESIAN_POINT('Ctrl Pts',(108.674600953806,8.86993971377894,10.4124583966274));
#104105=CARTESIAN_POINT('Ctrl Pts',(110.835008176012,8.60662167187442,10.5222565717328));
#104106=CARTESIAN_POINT('Ctrl Pts',(112.247929388326,10.2620217457998,10.6320547468382));
#104107=CARTESIAN_POINT('Ctrl Pts',(111.648540042177,12.354252174944,10.7418529219436));
#104108=CARTESIAN_POINT('Ctrl Pts',(109.573403926499,13.0103816274259,10.851651097049));
#104109=CARTESIAN_POINT('Ctrl Pts',(107.880149816284,11.6430534754381,10.9614492721544));
#104110=CARTESIAN_POINT('Ctrl Pts',(108.084551801994,9.47627808677931,11.0712474472598));
#104111=CARTESIAN_POINT('Ctrl Pts',(110.003632484133,8.44971825270481,11.1810456223652));
#104112=CARTESIAN_POINT('Ctrl Pts',(111.919461424199,9.48233397471366,11.2908437974706));
#104113=CARTESIAN_POINT('Ctrl Pts',(112.11701909216,11.6497441164658,11.400641972576));
#104114=CARTESIAN_POINT('Ctrl Pts',(110.419455011459,13.0117176675731,11.5104401476814));
#104115=CARTESIAN_POINT('Ctrl Pts',(108.34640149172,12.3490376097434,11.6202383227868));
#104116=CARTESIAN_POINT('Ctrl Pts',(107.753622996705,10.2549245762971,11.7300364978921));
#104117=CARTESIAN_POINT('Ctrl Pts',(109.171765395972,8.60399516008457,11.8398346729976));
#104118=CARTESIAN_POINT('Ctrl Pts',(111.33133019894,8.87413509358782,11.9496328481029));
#104119=CARTESIAN_POINT('Ctrl Pts',(112.299109453475,10.8235193461483,12.0594310232083));
#104120=CARTESIAN_POINT('Ctrl Pts',(111.208762519192,12.7070903445838,12.1692291983137));
#104121=CARTESIAN_POINT('Ctrl Pts',(109.036350749681,12.8387050721737,12.2790273734191));
#104122=CARTESIAN_POINT('Ctrl Pts',(107.726582214984,11.1005446949728,12.3888255485245));
#104123=CARTESIAN_POINT('Ctrl Pts',(108.451941481345,9.0485815134776,12.4986237236299));
#104124=CARTESIAN_POINT('Ctrl Pts',(110.563097171654,8.51970263038581,12.6084218987353));
#104125=CARTESIAN_POINT('Ctrl Pts',(112.170179054329,9.98734717223935,12.7182200738407));
#104126=CARTESIAN_POINT('Ctrl Pts',(111.83454756572,12.1377129436691,12.8280182489461));
#104127=CARTESIAN_POINT('Ctrl Pts',(109.856665808931,13.045806831973,12.9378164240515));
#104128=CARTESIAN_POINT('Ctrl Pts',(108.00707933468,11.8987582479109,13.0476145991569));
#104129=CARTESIAN_POINT('Ctrl Pts',(107.941554599805,9.7233042318488,13.1574127742623));
#104130=CARTESIAN_POINT('Ctrl Pts',(109.718654461597,8.46704452766819,13.2672109493676));
#104131=CARTESIAN_POINT('Ctrl Pts',(111.747738364555,9.25422104222753,13.377009124473));
#104132=CARTESIAN_POINT('Ctrl Pts',(112.212014332387,11.3808612270306,13.4868072995784));
#104133=CARTESIAN_POINT('Ctrl Pts',(110.696660157827,12.9418157250658,13.5966054746838));
#104134=CARTESIAN_POINT('Ctrl Pts',(108.556589694155,12.5426302847338,13.7064036497892));
#104135=CARTESIAN_POINT('Ctrl Pts',(107.710849413343,10.5347127971455,13.8162018248946));
#104136=CARTESIAN_POINT('Ctrl Pts',(108.510447412203,9.33175843476383,13.8894006082982));
#104137=CARTESIAN_POINT('Ctrl Pts',(109.07607384819,9.02823449157529,13.926));
#104138=CARTESIAN_POINT('Ctrl Pts',(111.057935419513,9.26763004755271,6.42661727848529));
#104139=CARTESIAN_POINT('Ctrl Pts',(111.544916735443,9.61517809513216,6.46321667018708));
#104140=CARTESIAN_POINT('Ctrl Pts',(112.141741037734,10.8219189981394,6.53641545359068));
#104141=CARTESIAN_POINT('Ctrl Pts',(111.122217137669,12.5780830812771,6.64621362869607));
#104142=CARTESIAN_POINT('Ctrl Pts',(109.096530351413,12.693818443993,6.75601180380146));
#104143=CARTESIAN_POINT('Ctrl Pts',(107.880381605119,11.0713981698394,6.86580997890686));
#104144=CARTESIAN_POINT('Ctrl Pts',(108.561303944473,9.16032755110486,6.97560815401225));
#104145=CARTESIAN_POINT('Ctrl Pts',(110.53030962347,8.6727681720058,7.08540632911764));
#104146=CARTESIAN_POINT('Ctrl Pts',(112.024499368246,10.044486639606,7.19520450422303));
#104147=CARTESIAN_POINT('Ctrl Pts',(111.706434380886,12.0478809876644,7.30500267932843));
#104148=CARTESIAN_POINT('Ctrl Pts',(109.860774497614,12.8893781246801,7.41480085443382));
#104149=CARTESIAN_POINT('Ctrl Pts',(108.139757896918,11.8157650188244,7.52459902953921));
#104150=CARTESIAN_POINT('Ctrl Pts',(108.083995052066,9.78808280640861,7.6343972046446));
#104151=CARTESIAN_POINT('Ctrl Pts',(109.74341191426,8.62150004593044,7.74419537975));
#104152=CARTESIAN_POINT('Ctrl Pts',(111.632521054667,9.3603133169554,7.85399355485539));
#104153=CARTESIAN_POINT('Ctrl Pts',(112.060224000132,11.3431535296936,7.96379172996079));
#104154=CARTESIAN_POINT('Ctrl Pts',(110.643646947998,12.7950113836044,8.07358990506617));
#104155=CARTESIAN_POINT('Ctrl Pts',(108.650887559929,12.4162080226842,8.18338808017156));
#104156=CARTESIAN_POINT('Ctrl Pts',(107.865832049491,10.5458416108559,8.29318625527696));
#104157=CARTESIAN_POINT('Ctrl Pts',(108.99124970855,8.85823462673231,8.40298443038235));
#104158=CARTESIAN_POINT('Ctrl Pts',(111.019684531805,8.86410580658457,8.51278260548774));
#104159=CARTESIAN_POINT('Ctrl Pts',(112.135314023955,10.5581994311237,8.62258078059314));
#104160=CARTESIAN_POINT('Ctrl Pts',(111.339444432452,12.4239898568863,8.73237895569853));
#104161=CARTESIAN_POINT('Ctrl Pts',(109.344525536706,12.7912512500102,8.84217713080392));
#104162=CARTESIAN_POINT('Ctrl Pts',(107.936376931771,11.3312170571891,8.95197530590931));
#104163=CARTESIAN_POINT('Ctrl Pts',(108.37555080575,9.35088662014198,9.0617734810147));
#104164=CARTESIAN_POINT('Ctrl Pts',(110.268905705914,8.62302017950486,9.1715716561201));
#104165=CARTESIAN_POINT('Ctrl Pts',(111.921540504384,9.79919217235273,9.28136983122548));
#104166=CARTESIAN_POINT('Ctrl Pts',(111.854042870886,11.8265121773396,9.39116800633089));
#104167=CARTESIAN_POINT('Ctrl Pts',(110.126835611168,12.8901556398784,9.50096618143627));
#104168=CARTESIAN_POINT('Ctrl Pts',(108.286087133963,12.0379658857068,9.61076435654167));
#104169=CARTESIAN_POINT('Ctrl Pts',(107.97960613622,10.0328095996804,9.72056253164706));
#104170=CARTESIAN_POINT('Ctrl Pts',(109.481749522078,8.66967072864468,9.83036070675245));
#104171=CARTESIAN_POINT('Ctrl Pts',(111.44782247533,9.16880946276298,9.94015888185785));
#104172=CARTESIAN_POINT('Ctrl Pts',(112.117827825647,11.0834047630663,10.0499570569632));
#104173=CARTESIAN_POINT('Ctrl Pts',(110.891987462706,12.699541433644,10.1597552320686));
#104174=CARTESIAN_POINT('Ctrl Pts',(108.867654140624,12.5704796867511,10.269553407174));
#104175=CARTESIAN_POINT('Ctrl Pts',(107.856978783287,10.8117535410786,10.3793515822794));
#104176=CARTESIAN_POINT('Ctrl Pts',(108.76470186133,8.99774660972897,10.4891497573848));
#104177=CARTESIAN_POINT('Ctrl Pts',(110.778244143576,8.75232898401329,10.5989479324902));
#104178=CARTESIAN_POINT('Ctrl Pts',(112.095114672999,10.2951946107433,10.7087461075956));
#104179=CARTESIAN_POINT('Ctrl Pts',(111.536471941391,12.2451947727408,10.818544282701));
#104180=CARTESIAN_POINT('Ctrl Pts',(109.602404017814,12.8567204062507,10.9283424578064));
#104181=CARTESIAN_POINT('Ctrl Pts',(108.024257680189,11.5823435112685,11.0381406329118));
#104182=CARTESIAN_POINT('Ctrl Pts',(108.214764375673,9.56286597187287,11.1479388080172));
#104183=CARTESIAN_POINT('Ctrl Pts',(110.003385547094,8.60609189246891,11.2577369831225));
#104184=CARTESIAN_POINT('Ctrl Pts',(111.788976030554,9.56851017926443,11.367535158228));
#104185=CARTESIAN_POINT('Ctrl Pts',(111.973103686457,11.5885793211039,11.4773333333333));
#104186=CARTESIAN_POINT('Ctrl Pts',(110.390940371052,12.857965622106,11.5871315084387));
#104187=CARTESIAN_POINT('Ctrl Pts',(108.458813468102,12.2403346947856,11.6969296835441));
#104188=CARTESIAN_POINT('Ctrl Pts',(107.906332180569,10.2885799083247,11.8067278586495));
#104189=CARTESIAN_POINT('Ctrl Pts',(109.228068959552,8.7498810230505,11.9165260337549));
#104190=CARTESIAN_POINT('Ctrl Pts',(111.240826090398,9.00165678673101,12.0263242088603));
#104191=CARTESIAN_POINT('Ctrl Pts',(112.142815506493,10.8185214854455,12.1361223839657));
#104192=CARTESIAN_POINT('Ctrl Pts',(111.126590587445,12.574046928972,12.2459205590711));
#104193=CARTESIAN_POINT('Ctrl Pts',(109.10185982956,12.6967144595395,12.3557187341765));
#104194=CARTESIAN_POINT('Ctrl Pts',(107.881129636909,11.0767145924571,12.4655169092819));
#104195=CARTESIAN_POINT('Ctrl Pts',(108.557178826907,9.16424430209567,12.5753150843872));
#104196=CARTESIAN_POINT('Ctrl Pts',(110.524817706812,8.67131871735124,12.6851132594926));
#104197=CARTESIAN_POINT('Ctrl Pts',(112.022649823154,10.0391924727959,12.794911434598));
#104198=CARTESIAN_POINT('Ctrl Pts',(111.709834634137,12.0433759242129,12.9047096097034));
#104199=CARTESIAN_POINT('Ctrl Pts',(109.866409697559,12.8897373978991,13.0145077848088));
#104200=CARTESIAN_POINT('Ctrl Pts',(108.142558503075,11.8206654192189,13.1243059599142));
#104201=CARTESIAN_POINT('Ctrl Pts',(108.081488153537,9.79309922734662,13.2341041350196));
#104202=CARTESIAN_POINT('Ctrl Pts',(109.737780390811,8.62224032359521,13.343902310125));
#104203=CARTESIAN_POINT('Ctrl Pts',(111.62892674083,9.35590441218188,13.4537004852304));
#104204=CARTESIAN_POINT('Ctrl Pts',(112.06164113016,11.3379751473697,13.5634986603358));
#104205=CARTESIAN_POINT('Ctrl Pts',(110.649301052932,12.7928156284369,13.6732968354412));
#104206=CARTESIAN_POINT('Ctrl Pts',(108.654713032074,12.4207668987791,13.7830950105466));
#104207=CARTESIAN_POINT('Ctrl Pts',(107.866466354452,10.5493480667357,13.892893185652));
#104208=CARTESIAN_POINT('Ctrl Pts',(108.61170751221,9.42817079637191,13.9660919690556));
#104209=CARTESIAN_POINT('Ctrl Pts',(109.13888254343,9.14528047504633,14.0026913607574));
#104210=CARTESIAN_POINT('Ctrl Pts',(110.980771099081,9.37575202541493,6.50330863924264));
#104211=CARTESIAN_POINT('Ctrl Pts',(111.432232683265,9.69795040758569,6.53990803094444));
#104212=CARTESIAN_POINT('Ctrl Pts',(111.985525460991,10.8166733276427,6.61310681434804));
#104213=CARTESIAN_POINT('Ctrl Pts',(111.040364199193,12.4447452743971,6.72290498945343));
#104214=CARTESIAN_POINT('Ctrl Pts',(109.162428155927,12.5520390626566,6.83270316455882));
#104215=CARTESIAN_POINT('Ctrl Pts',(108.034983587431,11.0479558397066,6.94250133966422));
#104216=CARTESIAN_POINT('Ctrl Pts',(108.666240409766,9.27627602202728,7.0522995147696));
#104217=CARTESIAN_POINT('Ctrl Pts',(110.491629585957,8.82427853778884,7.162097689875));
#104218=CARTESIAN_POINT('Ctrl Pts',(111.876835233855,10.0959457910871,7.27189586498039));
#104219=CARTESIAN_POINT('Ctrl Pts',(111.581969458989,11.953215375221,7.38169404008578));
#104220=CARTESIAN_POINT('Ctrl Pts',(109.870929409795,12.7333348954891,7.49149221519118));
#104221=CARTESIAN_POINT('Ctrl Pts',(108.275441337584,11.7380296184397,7.60129039029656));
#104222=CARTESIAN_POINT('Ctrl Pts',(108.223745756148,9.85824369258892,7.71108856540196));
#104223=CARTESIAN_POINT('Ctrl Pts',(109.762127088081,8.77674983666837,7.82088674050735));
#104224=CARTESIAN_POINT('Ctrl Pts',(111.51344726675,9.4616751076012,7.93068491561275));
#104225=CARTESIAN_POINT('Ctrl Pts',(111.909954161375,11.2998897461148,8.04048309071813));
#104226=CARTESIAN_POINT('Ctrl Pts',(110.596700245558,12.6458511316841,8.15028126582353));
#104227=CARTESIAN_POINT('Ctrl Pts',(108.749289922401,12.2946771547351,8.26007944092892));
#104228=CARTESIAN_POINT('Ctrl Pts',(108.021495255912,10.5607326364025,8.36987761603432));
#104229=CARTESIAN_POINT('Ctrl Pts',(109.064826534969,8.99621733035583,8.47967579113971));
#104230=CARTESIAN_POINT('Ctrl Pts',(110.945310177284,9.0016602746135,8.5894739662451));
#104231=CARTESIAN_POINT('Ctrl Pts',(111.979567224551,10.5721890946539,8.69927214135049));
#104232=CARTESIAN_POINT('Ctrl Pts',(111.241747240847,12.3018913929036,8.80907031645588));
#104233=CARTESIAN_POINT('Ctrl Pts',(109.392334921463,12.6423652569418,8.91886849156127));
#104234=CARTESIAN_POINT('Ctrl Pts',(108.086894693771,11.2888239031139,9.02866666666666));
#104235=CARTESIAN_POINT('Ctrl Pts',(108.494035843529,9.45293598078504,9.13846484177206));
#104236=CARTESIAN_POINT('Ctrl Pts',(110.249292102216,8.77815909383951,9.24826301687745));
#104237=CARTESIAN_POINT('Ctrl Pts',(111.781386044606,9.86854275701776,9.35806119198285));
#104238=CARTESIAN_POINT('Ctrl Pts',(111.718811593491,11.7479928943397,9.46785936708823));
#104239=CARTESIAN_POINT('Ctrl Pts',(110.117584400213,12.7340556998231,9.57765754219363));
#104240=CARTESIAN_POINT('Ctrl Pts',(108.41109752604,11.9440234668445,9.68745571729902));
#104241=CARTESIAN_POINT('Ctrl Pts',(108.126970820894,10.085120458018,9.79725389240441));
#104242=CARTESIAN_POINT('Ctrl Pts',(109.519549982488,8.82140701758676,9.90705206750981));
#104243=CARTESIAN_POINT('Ctrl Pts',(111.342220341822,9.28413927498756,10.0168502426152));
#104244=CARTESIAN_POINT('Ctrl Pts',(111.963356444935,11.059086688923,10.1266484177206));
#104245=CARTESIAN_POINT('Ctrl Pts',(110.826927152668,12.5573446254978,10.236446592826));
#104246=CARTESIAN_POINT('Ctrl Pts',(108.950245853805,12.4376964607659,10.3462447679314));
#104247=CARTESIAN_POINT('Ctrl Pts',(108.013287734483,10.8072493247118,10.4560429430368));
#104248=CARTESIAN_POINT('Ctrl Pts',(108.854802768855,9.12555350567899,10.5658411181422));
#104249=CARTESIAN_POINT('Ctrl Pts',(110.72148011114,8.89803629615216,10.6756392932476));
#104250=CARTESIAN_POINT('Ctrl Pts',(111.942299957671,10.3283674756868,10.7854374683529));
#104251=CARTESIAN_POINT('Ctrl Pts',(111.424403840605,12.1361373705376,10.8952356434583));
#104252=CARTESIAN_POINT('Ctrl Pts',(109.631404109129,12.7030591850754,11.0050338185637));
#104253=CARTESIAN_POINT('Ctrl Pts',(108.168365544094,11.5216335470989,11.1148319936691));
#104254=CARTESIAN_POINT('Ctrl Pts',(108.344976949352,9.64945385696643,11.2246301687745));
#104255=CARTESIAN_POINT('Ctrl Pts',(110.003138610054,8.76246553223299,11.3344283438799));
#104256=CARTESIAN_POINT('Ctrl Pts',(111.65849063691,9.6546863838152,11.4442265189853));
#104257=CARTESIAN_POINT('Ctrl Pts',(111.829188280755,11.527414525742,11.5540246940907));
#104258=CARTESIAN_POINT('Ctrl Pts',(110.362425730645,12.704213576639,11.6638228691961));
#104259=CARTESIAN_POINT('Ctrl Pts',(108.571225444483,12.1316317798277,11.7736210443015));
#104260=CARTESIAN_POINT('Ctrl Pts',(108.059041364434,10.3222352403522,11.8834192194069));
#104261=CARTESIAN_POINT('Ctrl Pts',(109.284372523132,8.89576688601643,11.9932173945123));
#104262=CARTESIAN_POINT('Ctrl Pts',(111.150321981855,9.12917847987418,12.1030155696177));
#104263=CARTESIAN_POINT('Ctrl Pts',(111.986521559511,10.8135236247426,12.212813744723));
#104264=CARTESIAN_POINT('Ctrl Pts',(111.044418655699,12.4410035133602,12.3226119198284));
#104265=CARTESIAN_POINT('Ctrl Pts',(109.167368909439,12.5547238469054,12.4324100949338));
#104266=CARTESIAN_POINT('Ctrl Pts',(108.035677058835,11.0528844899415,12.5422082700392));
#104267=CARTESIAN_POINT('Ctrl Pts',(108.662416172469,9.27990709071375,12.6520064451446));
#104268=CARTESIAN_POINT('Ctrl Pts',(110.48653824197,8.82293480431664,12.76180462025));
#104269=CARTESIAN_POINT('Ctrl Pts',(111.875120591979,10.0910377733525,12.8716027953554));
#104270=CARTESIAN_POINT('Ctrl Pts',(111.585121702554,11.9490389047567,12.9814009704608));
#104271=CARTESIAN_POINT('Ctrl Pts',(109.876153586188,12.7336679638252,13.0911991455662));
#104272=CARTESIAN_POINT('Ctrl Pts',(108.27803767147,11.7425725905269,13.2009973206716));
#104273=CARTESIAN_POINT('Ctrl Pts',(108.221421707269,9.86289422284445,13.310795495777));
#104274=CARTESIAN_POINT('Ctrl Pts',(109.756906320026,8.77743611952223,13.4205936708824));
#104275=CARTESIAN_POINT('Ctrl Pts',(111.510115117105,9.45758778213623,13.5303918459878));
#104276=CARTESIAN_POINT('Ctrl Pts',(111.911267927933,11.2950890677089,13.6401900210931));
#104277=CARTESIAN_POINT('Ctrl Pts',(110.601941948037,12.643815531808,13.7499881961985));
#104278=CARTESIAN_POINT('Ctrl Pts',(108.752836369992,12.2989035128244,13.8597863713039));
#104279=CARTESIAN_POINT('Ctrl Pts',(108.022083295562,10.5639833363259,13.9695845464093));
#104280=CARTESIAN_POINT('Ctrl Pts',(108.712967612216,9.52458315798,14.0427833298129));
#104281=CARTESIAN_POINT('Ctrl Pts',(109.20169123867,9.26232645851737,14.0793827215147));
#104282=CARTESIAN_POINT('Ctrl Pts',(110.90360677865,9.48387400327716,6.58));
#104283=CARTESIAN_POINT('Ctrl Pts',(111.319548631087,9.78072272003922,6.6165993917018));
#104284=CARTESIAN_POINT('Ctrl Pts',(111.829309884247,10.8114276571461,6.68979817510539));
#104285=CARTESIAN_POINT('Ctrl Pts',(110.958511260717,12.3114074675171,6.79959635021079));
#104286=CARTESIAN_POINT('Ctrl Pts',(109.228325960441,12.4102596813202,6.90939452531617));
#104287=CARTESIAN_POINT('Ctrl Pts',(108.189585569743,11.0245135095737,7.01919270042157));
#104288=CARTESIAN_POINT('Ctrl Pts',(108.771176875059,9.39222449294972,7.12899087552696));
#104289=CARTESIAN_POINT('Ctrl Pts',(110.452949548444,8.97578890357189,7.23878905063235));
#104290=CARTESIAN_POINT('Ctrl Pts',(111.729171099463,10.1474049425682,7.34858722573775));
#104291=CARTESIAN_POINT('Ctrl Pts',(111.457504537093,11.8585497627777,7.45838540084314));
#104292=CARTESIAN_POINT('Ctrl Pts',(109.881084321976,12.5772916662981,7.56818357594853));
#104293=CARTESIAN_POINT('Ctrl Pts',(108.41112477825,11.6602942180551,7.67798175105392));
#104294=CARTESIAN_POINT('Ctrl Pts',(108.36349646023,9.92840457876923,7.78777992615932));
#104295=CARTESIAN_POINT('Ctrl Pts',(109.780842261901,8.93199962740631,7.8975781012647));
#104296=CARTESIAN_POINT('Ctrl Pts',(111.394373478833,9.56303689824699,8.0073762763701));
#104297=CARTESIAN_POINT('Ctrl Pts',(111.759684322617,11.256625962536,8.11717445147549));
#104298=CARTESIAN_POINT('Ctrl Pts',(110.549753543119,12.4966908797639,8.22697262658089));
#104299=CARTESIAN_POINT('Ctrl Pts',(108.847692284874,12.1731462867861,8.33677080168627));
#104300=CARTESIAN_POINT('Ctrl Pts',(108.177158462332,10.5756236619491,8.44656897679167));
#104301=CARTESIAN_POINT('Ctrl Pts',(109.138403361389,9.13420003397936,8.55636715189706));
#104302=CARTESIAN_POINT('Ctrl Pts',(110.870935822764,9.13921474264243,8.66616532700245));
#104303=CARTESIAN_POINT('Ctrl Pts',(111.823820425147,10.5861787581841,8.77596350210785));
#104304=CARTESIAN_POINT('Ctrl Pts',(111.144050049243,12.179792928921,8.88576167721324));
#104305=CARTESIAN_POINT('Ctrl Pts',(109.440144306221,12.4934792638734,8.99555985231863));
#104306=CARTESIAN_POINT('Ctrl Pts',(108.237412455772,11.2464307490387,9.10535802742402));
#104307=CARTESIAN_POINT('Ctrl Pts',(108.612520881309,9.5549853414281,9.21515620252941));
#104308=CARTESIAN_POINT('Ctrl Pts',(110.229678498517,8.93329800817414,9.32495437763481));
#104309=CARTESIAN_POINT('Ctrl Pts',(111.641231584828,9.93789334168282,9.4347525527402));
#104310=CARTESIAN_POINT('Ctrl Pts',(111.583580316096,11.6694736113398,9.5445507278456));
#104311=CARTESIAN_POINT('Ctrl Pts',(110.108333189259,12.577955759768,9.65434890295098));
#104312=CARTESIAN_POINT('Ctrl Pts',(108.536107918118,11.8500810479822,9.76414707805638));
#104313=CARTESIAN_POINT('Ctrl Pts',(108.274335505568,10.1374313163555,9.87394525316177));
#104314=CARTESIAN_POINT('Ctrl Pts',(109.557350442899,8.97314330652884,9.98374342826716));
#104315=CARTESIAN_POINT('Ctrl Pts',(111.236618208315,9.39946908721214,10.0935416033726));
#104316=CARTESIAN_POINT('Ctrl Pts',(111.808885064222,11.0347686147797,10.2033397784779));
#104317=CARTESIAN_POINT('Ctrl Pts',(110.761866842631,12.4151478173515,10.3131379535833));
#104318=CARTESIAN_POINT('Ctrl Pts',(109.032837566985,12.3049132347807,10.4229361286887));
#104319=CARTESIAN_POINT('Ctrl Pts',(108.169596685679,10.802745108345,10.5327343037941));
#104320=CARTESIAN_POINT('Ctrl Pts',(108.944903676379,9.25336040162902,10.6425324788995));
#104321=CARTESIAN_POINT('Ctrl Pts',(110.664716078704,9.04374360829103,10.7523306540049));
#104322=CARTESIAN_POINT('Ctrl Pts',(111.789485242344,10.3615403406303,10.8621288291103));
#104323=CARTESIAN_POINT('Ctrl Pts',(111.312335739819,12.0270799683344,10.9719270042157));
#104324=CARTESIAN_POINT('Ctrl Pts',(109.660404200444,12.5493979639002,11.0817251793211));
#104325=CARTESIAN_POINT('Ctrl Pts',(108.312473407999,11.4609235829293,11.1915233544265));
#104326=CARTESIAN_POINT('Ctrl Pts',(108.475189523031,9.73604174205998,11.3013215295319));
#104327=CARTESIAN_POINT('Ctrl Pts',(110.002891673014,8.91883917199709,11.4111197046373));
#104328=CARTESIAN_POINT('Ctrl Pts',(111.528005243266,9.74086258836599,11.5209178797427));
#104329=CARTESIAN_POINT('Ctrl Pts',(111.685272875053,11.4662497303801,11.630716054848));
#104330=CARTESIAN_POINT('Ctrl Pts',(110.333911090238,12.5504615311719,11.7405142299534));
#104331=CARTESIAN_POINT('Ctrl Pts',(108.683637420865,12.0229288648699,11.8503124050588));
#104332=CARTESIAN_POINT('Ctrl Pts',(108.211750548298,10.3558905723798,11.9601105801642));
#104333=CARTESIAN_POINT('Ctrl Pts',(109.340676086711,9.04165274898235,12.0699087552696));
#104334=CARTESIAN_POINT('Ctrl Pts',(111.059817873312,9.25670017301735,12.179706930375));
#104335=CARTESIAN_POINT('Ctrl Pts',(111.830227612529,10.8085257640398,12.2895051054804));
#104336=CARTESIAN_POINT('Ctrl Pts',(110.962246723952,12.3079600977483,12.3993032805858));
#104337=CARTESIAN_POINT('Ctrl Pts',(109.232877989319,12.4127332342713,12.5091014556912));
#104338=CARTESIAN_POINT('Ctrl Pts',(108.190224480761,11.0290543874259,12.6188996307966));
#104339=CARTESIAN_POINT('Ctrl Pts',(108.76765351803,9.39556987933182,12.728697805902));
#104340=CARTESIAN_POINT('Ctrl Pts',(110.448258777128,8.97455089128206,12.8384959810074));
#104341=CARTESIAN_POINT('Ctrl Pts',(111.727591360803,10.1428830739091,12.9482941561128));
#104342=CARTESIAN_POINT('Ctrl Pts',(111.460408770971,11.8547018853006,13.0580923312181));
#104343=CARTESIAN_POINT('Ctrl Pts',(109.885897474817,12.5775985297513,13.1678905063236));
#104344=CARTESIAN_POINT('Ctrl Pts',(108.413516839864,11.6644797618349,13.2776886814289));
#104345=CARTESIAN_POINT('Ctrl Pts',(108.361355261002,9.93268921834226,13.3874868565343));
#104346=CARTESIAN_POINT('Ctrl Pts',(109.77603224924,8.93263191544926,13.4972850316397));
#104347=CARTESIAN_POINT('Ctrl Pts',(111.391303493381,9.55927115209057,13.6070832067451));
#104348=CARTESIAN_POINT('Ctrl Pts',(111.760894725706,11.2522029880481,13.7168813818505));
#104349=CARTESIAN_POINT('Ctrl Pts',(110.554582843142,12.4948154351791,13.8266795569559));
#104350=CARTESIAN_POINT('Ctrl Pts',(108.850959707911,12.1770401268697,13.9364777320613));
#104351=CARTESIAN_POINT('Ctrl Pts',(108.177700236671,10.578618605916,14.0462759071667));
#104352=CARTESIAN_POINT('Ctrl Pts',(108.814227712222,9.62099551958808,14.1194746905703));
#104353=CARTESIAN_POINT('Ctrl Pts',(109.264499933909,9.37937244198841,14.1560740822721));
#104354=CARTESIAN_POINT('Ctrl Pts',(109.07607384819,9.02823449157531,13.926));
#104355=CARTESIAN_POINT('Ctrl Pts',(108.510447412203,9.33175843476385,13.8894006082982));
#104356=CARTESIAN_POINT('Ctrl Pts',(108.110648412773,9.9332356159547,13.8528012165964));
#104357=CARTESIAN_POINT('Ctrl Pts',(108.051705626527,10.5686271211482,13.8162018248946));
#104358=CARTESIAN_POINT('Ctrl Pts',(108.04615904351,10.6284181822157,13.8127577806378));
#104359=CARTESIAN_POINT('Ctrl Pts',(108.043630750232,10.6885095554155,13.809313736381));
#104360=CARTESIAN_POINT('Ctrl Pts',(108.04401647614,10.7486495636155,13.8058696921242));
#104361=CARTESIAN_POINT('Origin',(110.,10.75,6.58));
#104362=CARTESIAN_POINT('',(107.846,10.75,6.38));
#104363=CARTESIAN_POINT('Origin',(110.,10.75,6.38));
#104364=CARTESIAN_POINT('Origin',(107.846,10.75,6.58));
#104365=CARTESIAN_POINT('Origin',(112.,10.75,6.38));
#104366=CARTESIAN_POINT('',(106.5,10.75,6.38));
#104367=CARTESIAN_POINT('Origin',(110.,10.75,6.38));
#104368=CARTESIAN_POINT('Origin',(110.,10.75,10.13));
#104369=CARTESIAN_POINT('Origin',(110.,10.75,13.926));
#104370=CARTESIAN_POINT('Origin',(114.,11.35,3.78));
#104371=CARTESIAN_POINT('',(113.448187929913,11.35,4.88));
#104372=CARTESIAN_POINT('',(113.448187929913,11.35,4.18));
#104373=CARTESIAN_POINT('',(113.448187929913,11.35,5.28));
#104374=CARTESIAN_POINT('',(106.551812070087,11.35,4.88));
#104375=CARTESIAN_POINT('',(114.,11.35,4.88));
#104376=CARTESIAN_POINT('',(106.551812070087,11.35,4.18));
#104377=CARTESIAN_POINT('',(106.551812070087,11.35,5.28));
#104378=CARTESIAN_POINT('',(106.958618734851,11.35,3.78));
#104379=CARTESIAN_POINT('Ctrl Pts',(106.958618734851,11.35,3.78));
#104380=CARTESIAN_POINT('Ctrl Pts',(106.767542877162,11.35,3.96746275283796));
#104381=CARTESIAN_POINT('Ctrl Pts',(106.551812070087,11.35,4.18));
#104382=CARTESIAN_POINT('',(113.041381265149,11.35,3.78));
#104383=CARTESIAN_POINT('',(113.55,11.35,3.78));
#104384=CARTESIAN_POINT('Ctrl Pts',(113.448187929913,11.35,4.18));
#104385=CARTESIAN_POINT('Ctrl Pts',(113.232457122838,11.35,3.96746275283796));
#104386=CARTESIAN_POINT('Ctrl Pts',(113.041381265149,11.35,3.78));
#104387=CARTESIAN_POINT('Origin',(106.,10.15,3.78));
#104388=CARTESIAN_POINT('',(113.448187929913,10.15,4.18));
#104389=CARTESIAN_POINT('',(113.448187929913,10.15,4.88));
#104390=CARTESIAN_POINT('',(113.448187929913,10.15,5.28));
#104391=CARTESIAN_POINT('',(113.041381265149,10.15,3.78));
#104392=CARTESIAN_POINT('Ctrl Pts',(113.041381265149,10.15,3.78));
#104393=CARTESIAN_POINT('Ctrl Pts',(113.232457122844,10.15,3.96746275284386));
#104394=CARTESIAN_POINT('Ctrl Pts',(113.448187929913,10.15,4.18));
#104395=CARTESIAN_POINT('',(106.958618734851,10.15,3.78));
#104396=CARTESIAN_POINT('',(109.55,10.15,3.78));
#104397=CARTESIAN_POINT('',(106.551812070087,10.15,4.18));
#104398=CARTESIAN_POINT('Ctrl Pts',(106.551812070087,10.15,4.18));
#104399=CARTESIAN_POINT('Ctrl Pts',(106.767542877156,10.15,3.96746275284386));
#104400=CARTESIAN_POINT('Ctrl Pts',(106.958618734851,10.15,3.78));
#104401=CARTESIAN_POINT('',(106.551812070087,10.15,4.88));
#104402=CARTESIAN_POINT('',(106.551812070087,10.15,5.28));
#104403=CARTESIAN_POINT('',(106.,10.15,4.88));
#104404=CARTESIAN_POINT('Origin',(110.,10.75,4.88));
#104405=CARTESIAN_POINT('Origin',(110.,10.75,4.88));
#104406=CARTESIAN_POINT('',(106.5,10.75,4.88));
#104407=CARTESIAN_POINT('Origin',(110.,10.75,4.88));
#104408=CARTESIAN_POINT('Origin',(110.,10.75,4.88));
#104409=CARTESIAN_POINT('Origin',(110.,10.75,3.98));
#104410=CARTESIAN_POINT('Origin',(110.,10.75,4.18));
#104411=CARTESIAN_POINT('Origin',(110.,10.75,3.78));
#104412=CARTESIAN_POINT('Origin',(110.,10.75,3.98));
#104413=CARTESIAN_POINT('Origin',(110.,10.75,3.78));
#104414=CARTESIAN_POINT('Origin',(110.,10.75,4.18));
#104415=CARTESIAN_POINT('Origin',(113.1,10.75,3.78));
#104416=CARTESIAN_POINT('Origin',(113.1,10.75,3.78));
#104417=CARTESIAN_POINT('Origin',(110.,10.75,5.28));
#104418=CARTESIAN_POINT('',(106.5,10.75,5.28));
#104419=CARTESIAN_POINT('Origin',(110.,10.75,14.13));
#104420=CARTESIAN_POINT('',(108.5,10.75,14.38));
#104421=CARTESIAN_POINT('Origin',(110.,10.75,14.38));
#104422=CARTESIAN_POINT('',(108.25,10.75,14.13));
#104423=CARTESIAN_POINT('Origin',(110.,10.75,14.38));
#113956=UNCERTAINTY_MEASURE_WITH_UNIT(LENGTH_MEASURE(0.01),#113985,
'DISTANCE_ACCURACY_VALUE',
'Maximum model space distance between geometric entities at asserted c
onnectivities');
#113964=UNCERTAINTY_MEASURE_WITH_UNIT(LENGTH_MEASURE(0.01),#113985,
'DISTANCE_ACCURACY_VALUE',
'Maximum model space distance between geometric entities at asserted c
onnectivities');
#113976=(
GEOMETRIC_REPRESENTATION_CONTEXT(3)
GLOBAL_UNCERTAINTY_ASSIGNED_CONTEXT((#113956))
GLOBAL_UNIT_ASSIGNED_CONTEXT((#113985,#113987,#113988))
REPRESENTATION_CONTEXT('','3D')
);
#113984=(
GEOMETRIC_REPRESENTATION_CONTEXT(3)
GLOBAL_UNCERTAINTY_ASSIGNED_CONTEXT((#113964))
GLOBAL_UNIT_ASSIGNED_CONTEXT((#113985,#113987,#113988))
REPRESENTATION_CONTEXT('','3D')
);
#113985=(
LENGTH_UNIT()
NAMED_UNIT(*)
SI_UNIT(.MILLI.,.METRE.)
);
#113987=(
NAMED_UNIT(*)
PLANE_ANGLE_UNIT()
SI_UNIT($,.RADIAN.)
);
#113988=(
NAMED_UNIT(*)
SI_UNIT($,.STERADIAN.)
SOLID_ANGLE_UNIT()
);
#114000=SHAPE_DEFINITION_REPRESENTATION(#114019,#114062);
#114019=PRODUCT_DEFINITION_SHAPE('',$,#114082);
#114062=SHAPE_REPRESENTATION('',(#63058),#113976);
#114070=PRODUCT_DEFINITION_CONTEXT('part definition',#114129,'design');
#114082=PRODUCT_DEFINITION('2026-10-05-09-51-16-067',
'ISO 1207 - M4 x 8 - 4.8 (Lock Clamp Screw, slotted cheese head)',#114101,
#114070);
#114101=PRODUCT_DEFINITION_FORMATION('',$,#114142);
#114129=APPLICATION_CONTEXT(
'Core Data for Automotive Mechanical Design Process');
#114130=PRODUCT_CONTEXT('part definition',#114129,'mechanical');
#114142=PRODUCT('2026-10-05-09-51-16-067',
'ISO 1207 - M4 x 8 - 4.8 (Lock Clamp Screw, slotted cheese head)',$,(#114130));
#114311=COLOUR_RGB('Black',0.12,0.14,0.17);
#114312=FILL_AREA_STYLE_COLOUR('',#114311);
#114313=FILL_AREA_STYLE('',(#114312));
#114314=SURFACE_STYLE_FILL_AREA(#114313);
#114315=SURFACE_SIDE_STYLE('',(#114314));
#114316=SURFACE_STYLE_USAGE(.BOTH.,#114315);
#114317=PRESENTATION_STYLE_ASSIGNMENT((#114316));
ENDSEC;
END-ISO-10303-21;
